ISO-10303-21;
HEADER;
/* Generated by software containing ST-Developer
 * from STEP Tools, Inc. (www.steptools.com) 
 */

FILE_DESCRIPTION(
/* description */ ('STEP AP214'),
/* implementation_level */ '2;1');

FILE_NAME(
/* name */ 'hex flange nut gradea_iso_ISO - 4161 - M12 - N.step',
/* time_stamp */ '2026-11-04T19:54:22-08:00',
/* author */ (''),
/* organization */ (''),
/* preprocessor_version */ 'ST-DEVELOPER v20.2',
/* originating_system */ 'Autodesk Translation Framework v15.17.0.0',
/* authorisation */ '');

FILE_SCHEMA (('AUTOMOTIVE_DESIGN { 1 0 10303 214 3 1 1 }'));
ENDSEC;

DATA;
#10=MECHANICAL_DESIGN_GEOMETRIC_PRESENTATION_REPRESENTATION('',(#246),#14084);
#52=CONICAL_SURFACE('',#3807,6.,0.959931088596879);
#53=CONICAL_SURFACE('',#3810,5.01,0.959931088596881);
#54=CONICAL_SURFACE('',#3813,12.389406481562,1.22173047639605);
#55=CONICAL_SURFACE('',#3834,9.,0.85944549144248);
#56=CONICAL_SURFACE('',#3835,9.,0.85944549144248);
#57=CONICAL_SURFACE('',#3836,9.,0.85944549144248);
#58=CONICAL_SURFACE('',#3837,9.,0.85944549144248);
#59=CONICAL_SURFACE('',#3838,9.,0.85944549144248);
#60=CONICAL_SURFACE('',#3839,9.,0.85944549144248);
#65=(
BOUNDED_SURFACE()
B_SPLINE_SURFACE(3,2,((#13700,#13701,#13702),(#13703,#13704,#13705),(#13706,
#13707,#13708),(#13709,#13710,#13711),(#13712,#13713,#13714),(#13715,#13716,
#13717),(#13718,#13719,#13720),(#13721,#13722,#13723)),.UNSPECIFIED.,.F.,
 .F.,.F.)
B_SPLINE_SURFACE_WITH_KNOTS((4,2,2,4),(3,3),(0.0461385444250929,0.0516992567704878,
0.0544796129431853,0.0572599691158828),(0.,1.00002275764424),
 .UNSPECIFIED.)
GEOMETRIC_REPRESENTATION_ITEM()
RATIONAL_B_SPLINE_SURFACE(((1.,0.804773725708204,1.00000888578019),(1.,
0.812372242905555,1.00000853993149),(1.,0.819062000811371,1.00000823544523),
(1.,0.819189579699543,1.00000822963844),(1.,0.817605054849148,1.00000830175855),
(1.,0.812291861790874,1.00000854359006),(1.,0.808626740000292,1.00000871040914),
(1.,0.804766788192626,1.00000888609596)))
REPRESENTATION_ITEM('')
SURFACE()
);
#66=(
BOUNDED_SURFACE()
B_SPLINE_SURFACE(3,2,((#13786,#13787,#13788),(#13789,#13790,#13791),(#13792,
#13793,#13794),(#13795,#13796,#13797),(#13798,#13799,#13800),(#13801,#13802,
#13803),(#13804,#13805,#13806),(#13807,#13808,#13809)),.UNSPECIFIED.,.F.,
 .F.,.F.)
B_SPLINE_SURFACE_WITH_KNOTS((4,2,2,4),(3,3),(0.0461385444250929,0.0516992567704878,
0.0544796129431853,0.0572599691158827),(0.,1.00002275764377),
 .UNSPECIFIED.)
GEOMETRIC_REPRESENTATION_ITEM()
RATIONAL_B_SPLINE_SURFACE(((1.,0.804773725708297,1.00000888578001),(1.,
0.812372242905804,1.00000853993131),(1.,0.819062000811241,1.00000823544506),
(1.,0.819189579699735,1.00000822963827),(1.,0.817605054849233,1.00000830175837),
(1.,0.812291861790962,1.00000854358988),(1.,0.808626740000384,1.00000871040896),
(1.,0.804766788192718,1.00000888609577)))
REPRESENTATION_ITEM('')
SURFACE()
);
#67=(
BOUNDED_SURFACE()
B_SPLINE_SURFACE(3,2,((#13841,#13842,#13843),(#13844,#13845,#13846),(#13847,
#13848,#13849),(#13850,#13851,#13852),(#13853,#13854,#13855),(#13856,#13857,
#13858),(#13859,#13860,#13861),(#13862,#13863,#13864)),.UNSPECIFIED.,.F.,
 .F.,.F.)
B_SPLINE_SURFACE_WITH_KNOTS((4,2,2,4),(3,3),(0.0460112723212199,0.0515724236699156,
0.0543529993442635,0.0571335750186114),(0.,1.),.UNSPECIFIED.)
GEOMETRIC_REPRESENTATION_ITEM()
RATIONAL_B_SPLINE_SURFACE(((1.,0.804778149799748,1.),(1.,0.812377089679977,
1.),(1.,0.819066896577867,1.),(1.,0.81919332893791,1.),(1.,0.817608725913226,
1.),(1.,0.812295770981002,1.),(1.,0.808630931896093,1.),(1.,0.804771243949043,
1.)))
REPRESENTATION_ITEM('')
SURFACE()
);
#68=(
BOUNDED_SURFACE()
B_SPLINE_SURFACE(3,2,((#13896,#13897,#13898),(#13899,#13900,#13901),(#13902,
#13903,#13904),(#13905,#13906,#13907),(#13908,#13909,#13910),(#13911,#13912,
#13913),(#13914,#13915,#13916),(#13917,#13918,#13919)),.UNSPECIFIED.,.F.,
 .F.,.F.)
B_SPLINE_SURFACE_WITH_KNOTS((4,2,2,4),(3,3),(0.0459959130509696,0.0515565609914623,
0.0543368849617087,0.0571172089319551),(0.,1.00002218942476),
 .UNSPECIFIED.)
GEOMETRIC_REPRESENTATION_ITEM()
RATIONAL_B_SPLINE_SURFACE(((1.,0.804773845337407,1.00000866391214),(1.,
0.812372128424595,1.00000832670908),(1.,0.819061503960629,1.00000802984229),
(1.,0.81918996388213,1.00000802414138),(1.,0.81760551996088,1.00000809445718),
(1.,0.812292231605809,1.00000833025481),(1.,0.80862696186913,1.00000849291526),
(1.,0.804766890162773,1.0000086642208)))
REPRESENTATION_ITEM('')
SURFACE()
);
#69=(
BOUNDED_SURFACE()
B_SPLINE_SURFACE(3,2,((#13951,#13952,#13953),(#13954,#13955,#13956),(#13957,
#13958,#13959),(#13960,#13961,#13962),(#13963,#13964,#13965),(#13966,#13967,
#13968),(#13969,#13970,#13971),(#13972,#13973,#13974)),.UNSPECIFIED.,.F.,
 .F.,.F.)
B_SPLINE_SURFACE_WITH_KNOTS((4,2,2,4),(3,3),(0.0461385444250929,0.0516992567704878,
0.0544796129431853,0.0572599691158827),(0.,1.00002275764329),
 .UNSPECIFIED.)
GEOMETRIC_REPRESENTATION_ITEM()
RATIONAL_B_SPLINE_SURFACE(((1.,0.804773725708389,1.00000888577982),(1.,
0.812372242905893,1.00000853993114),(1.,0.819062000811328,1.00000823544489),
(1.,0.819189579699822,1.0000082296381),(1.,0.817605054849161,1.0000083017582),
(1.,0.812291861791211,1.00000854358971),(1.,0.808626740000355,1.00000871040877),
(1.,0.804766788192811,1.00000888609559)))
REPRESENTATION_ITEM('')
SURFACE()
);
#70=(
BOUNDED_SURFACE()
B_SPLINE_SURFACE(3,2,((#14006,#14007,#14008),(#14009,#14010,#14011),(#14012,
#14013,#14014),(#14015,#14016,#14017),(#14018,#14019,#14020),(#14021,#14022,
#14023),(#14024,#14025,#14026),(#14027,#14028,#14029)),.UNSPECIFIED.,.F.,
 .F.,.F.)
B_SPLINE_SURFACE_WITH_KNOTS((4,2,2,4),(3,3),(0.0461385444250929,0.0516992567704878,
0.0544796129431853,0.0572599691158827),(0.,1.00002275764337),
 .UNSPECIFIED.)
GEOMETRIC_REPRESENTATION_ITEM()
RATIONAL_B_SPLINE_SURFACE(((1.,0.804773725708374,1.00000888577985),(1.,
0.812372242905718,1.00000853993116),(1.,0.819062000811528,1.00000823544491),
(1.,0.8191895796997,1.00000822963813),(1.,0.817605054849307,1.00000830175823),
(1.,0.812291861791037,1.00000854358973),(1.,0.80862674000046,1.0000087104088),
(1.,0.804766788192796,1.00000888609562)))
REPRESENTATION_ITEM('')
SURFACE()
);
#72=TOROIDAL_SURFACE('',#3816,12.0720179162868,0.927982083713184);
#131=B_SPLINE_CURVE_WITH_KNOTS('',3,(#13305,#13306,#13307,#13308,#13309,
#13310),.UNSPECIFIED.,.F.,.F.,(4,2,4),(0.00553837226488889,0.00830239406258802,
0.0110664158602872),.UNSPECIFIED.);
#132=B_SPLINE_CURVE_WITH_KNOTS('',3,(#13312,#13313,#13314,#13315,#13316,
#13317,#13318,#13319,#13320,#13321),.UNSPECIFIED.,.F.,.F.,(4,2,2,2,4),(0.,
0.00276660396507179,0.00553320793014358,0.00829981189521537,0.0110664158602872),
 .UNSPECIFIED.);
#133=B_SPLINE_CURVE_WITH_KNOTS('',3,(#13323,#13324,#13325,#13326,#13327,
#13328,#13329,#13330,#13331,#13332),.UNSPECIFIED.,.F.,.F.,(4,2,2,2,4),(1.62072509839964E-19,
0.00276660396507179,0.00553320793014358,0.00829981189521537,0.0110664158602872),
 .UNSPECIFIED.);
#134=B_SPLINE_CURVE_WITH_KNOTS('',3,(#13334,#13335,#13336,#13337,#13338,
#13339,#13340,#13341,#13342,#13343,#13344,#13345,#13346,#13347,#13348,#13349,
#13350,#13351,#13352,#13353,#13354,#13355),.UNSPECIFIED.,.F.,.F.,(4,3,3,
3,3,3,3,4),(0.,0.00114977203808909,0.00217838054954922,0.00274980879509083,
0.00276918613244445,0.00408374644507523,0.00535443888579874,0.0055383722648889),
 .UNSPECIFIED.);
#135=B_SPLINE_CURVE_WITH_KNOTS('',3,(#13357,#13358,#13359,#13360,#13361,
#13362),.UNSPECIFIED.,.F.,.F.,(4,2,4),(0.0055383722648889,0.00830239406258803,
0.0110664158602872),.UNSPECIFIED.);
#136=B_SPLINE_CURVE_WITH_KNOTS('',3,(#13364,#13365,#13366,#13367,#13368,
#13369,#13370,#13371,#13372,#13373),.UNSPECIFIED.,.F.,.F.,(4,2,2,2,4),(0.,
0.00276660396507179,0.00553320793014358,0.00829981189521537,0.0110664158602872),
 .UNSPECIFIED.);
#137=B_SPLINE_CURVE_WITH_KNOTS('',3,(#13375,#13376,#13377,#13378,#13379,
#13380,#13381,#13382,#13383,#13384),.UNSPECIFIED.,.F.,.F.,(4,2,2,2,4),(0.,
0.00276660396507179,0.00553320793014358,0.00829981189521537,0.0110664158602872),
 .UNSPECIFIED.);
#138=B_SPLINE_CURVE_WITH_KNOTS('',3,(#13385,#13386,#13387,#13388,#13389,
#13390),.UNSPECIFIED.,.F.,.F.,(4,2,4),(0.,0.00276918613244445,0.00553837226488889),
 .UNSPECIFIED.);
#139=B_SPLINE_CURVE_WITH_KNOTS('',3,(#13403,#13404,#13405,#13406,#13407,
#13408,#13409,#13410,#13411,#13412,#13413,#13414,#13415,#13416,#13417,#13418,
#13419,#13420,#13421,#13422,#13423,#13424,#13425,#13426,#13427,#13428,#13429,
#13430,#13431,#13432,#13433,#13434,#13435,#13436,#13437,#13438,#13439),
 .UNSPECIFIED.,.F.,.F.,(4,3,3,3,3,3,3,3,3,3,3,3,4),(0.,0.00104332150239121,
0.00206065848340059,0.00259807621135332,0.00371876749530484,0.00484862102586553,
0.00515636113902887,0.00519615242270663,0.00700298769703306,0.00779422863405995,
0.00803596165391469,0.00922538326593667,0.0103923048454133),
 .UNSPECIFIED.);
#140=B_SPLINE_CURVE_WITH_KNOTS('',3,(#13453,#13454,#13455,#13456,#13457,
#13458,#13459,#13460,#13461,#13462,#13463,#13464,#13465,#13466,#13467,#13468,
#13469,#13470,#13471,#13472,#13473,#13474,#13475,#13476,#13477,#13478,#13479,
#13480,#13481,#13482,#13483,#13484,#13485,#13486,#13487,#13488,#13489),
 .UNSPECIFIED.,.F.,.F.,(4,3,3,3,3,3,3,3,3,3,3,3,4),(0.,0.00104332150241254,
0.00206065848345604,0.00259807621135332,0.00371876749530863,0.00484862102596152,
0.00515636113902889,0.00519615242270663,0.00700298769762406,0.00779422863405995,
0.00803596165391469,0.00922538326592427,0.0103923048454133),
 .UNSPECIFIED.);
#141=B_SPLINE_CURVE_WITH_KNOTS('',3,(#13501,#13502,#13503,#13504,#13505,
#13506,#13507,#13508,#13509,#13510,#13511,#13512,#13513,#13514,#13515,#13516,
#13517,#13518,#13519,#13520,#13521,#13522,#13523,#13524,#13525,#13526,#13527,
#13528,#13529,#13530,#13531,#13532,#13533,#13534,#13535,#13536,#13537),
 .UNSPECIFIED.,.F.,.F.,(4,3,3,3,3,3,3,3,3,3,3,3,4),(0.,0.00104353079945368,
0.0020610675491746,0.00259807621135332,0.00371858000064792,0.00484809657734561,
0.00515608341291941,0.00519615242270663,0.00716112156284184,0.00779422863405995,
0.00803585117301137,0.00922121712355728,0.0103923048454133),
 .UNSPECIFIED.);
#142=B_SPLINE_CURVE_WITH_KNOTS('',3,(#13549,#13550,#13551,#13552,#13553,
#13554,#13555,#13556,#13557,#13558,#13559,#13560,#13561,#13562,#13563,#13564,
#13565,#13566,#13567,#13568,#13569,#13570,#13571,#13572,#13573,#13574,#13575,
#13576,#13577,#13578,#13579,#13580,#13581,#13582,#13583,#13584,#13585),
 .UNSPECIFIED.,.F.,.F.,(4,3,3,3,3,3,3,3,3,3,3,3,4),(0.,0.00104332150237409,
0.00206065848338429,0.00259807621135332,0.00371876749530815,0.00484862102586396,
0.00515636113902887,0.00519615242270663,0.00700298769768474,0.00779422863405995,
0.0080359616539147,0.00922538326598745,0.0103923048454133),
 .UNSPECIFIED.);
#143=B_SPLINE_CURVE_WITH_KNOTS('',3,(#13597,#13598,#13599,#13600,#13601,
#13602,#13603,#13604,#13605,#13606,#13607,#13608,#13609,#13610,#13611,#13612,
#13613,#13614,#13615,#13616,#13617,#13618,#13619,#13620,#13621,#13622,#13623,
#13624,#13625,#13626,#13627,#13628,#13629,#13630,#13631,#13632,#13633),
 .UNSPECIFIED.,.F.,.F.,(4,3,3,3,3,3,3,3,3,3,3,3,4),(0.,0.001043321502395,
0.00206065848341437,0.00259807621135332,0.00371876749539627,0.00484862102602629,
0.00515636113902888,0.00519615242270663,0.00700298769718223,0.00779422863405995,
0.00803596165391469,0.00922538326593071,0.0103923048454133),
 .UNSPECIFIED.);
#144=B_SPLINE_CURVE_WITH_KNOTS('',3,(#13642,#13643,#13644,#13645,#13646,
#13647,#13648,#13649,#13650,#13651,#13652,#13653,#13654,#13655,#13656,#13657,
#13658,#13659,#13660,#13661,#13662,#13663,#13664,#13665,#13666,#13667,#13668,
#13669,#13670,#13671,#13672,#13673,#13674,#13675,#13676,#13677,#13678),
 .UNSPECIFIED.,.F.,.F.,(4,3,3,3,3,3,3,3,3,3,3,3,4),(0.,0.0010434213010507,
0.00206085463009113,0.00259807621135332,0.0037190935981022,0.0048493549766946,
0.0051567201755677,0.00519615242270663,0.00684590372399744,0.00779422863405995,
0.00803611110738811,0.009229743876539,0.0103923048454133),.UNSPECIFIED.);
#145=B_SPLINE_CURVE_WITH_KNOTS('',3,(#13724,#13725,#13726,#13727,#13728,
#13729,#13730,#13731,#13732,#13733,#13734,#13735,#13736,#13737,#13738,#13739,
#13740,#13741,#13742,#13743,#13744,#13745,#13746,#13747,#13748,#13749,#13750,
#13751,#13752,#13753,#13754),.UNSPECIFIED.,.F.,.F.,(4,3,3,3,3,3,3,3,3,3,
4),(-5.63655962566362E-6,0.000138968027467558,0.000300786513285965,0.000418320464104159,
0.000498923906492782,0.000607102007354961,0.000706192487495778,0.000797150264455975,
0.000884559431233306,0.00096812822464727,0.00100346392791823),
 .UNSPECIFIED.);
#146=B_SPLINE_CURVE_WITH_KNOTS('',3,(#13755,#13756,#13757,#13758,#13759,
#13760,#13761,#13762,#13763,#13764,#13765,#13766,#13767,#13768,#13769,#13770,
#13771,#13772,#13773,#13774,#13775,#13776,#13777,#13778,#13779,#13780,#13781,
#13782,#13783,#13784,#13785),.UNSPECIFIED.,.F.,.F.,(4,3,3,3,3,3,3,3,3,3,
4),(2.03723854135766E-8,8.34362348219312E-5,0.000169714573606459,0.000262192398767452,
0.000359257400005965,0.000466160307363708,0.000502785923637984,0.000616382138541576,
0.0007569494209109,0.000924038166163904,0.00100557184727597),
 .UNSPECIFIED.);
#147=B_SPLINE_CURVE_WITH_KNOTS('',3,(#13810,#13811,#13812,#13813,#13814,
#13815,#13816,#13817,#13818,#13819,#13820,#13821,#13822,#13823,#13824,#13825,
#13826,#13827,#13828,#13829,#13830,#13831,#13832,#13833,#13834,#13835,#13836,
#13837,#13838,#13839,#13840),.UNSPECIFIED.,.F.,.F.,(4,3,3,3,3,3,3,3,3,3,
4),(2.03923073170011E-8,8.34362553594438E-5,0.000169714594923251,0.000262192421030851,
0.000359257423499574,0.000466160332015168,0.000502785923637989,0.000616382138542073,
0.000756949420907432,0.000924038166154207,0.00100557184727598),
 .UNSPECIFIED.);
#148=B_SPLINE_CURVE_WITH_KNOTS('',3,(#13865,#13866,#13867,#13868,#13869,
#13870,#13871,#13872,#13873,#13874,#13875,#13876,#13877,#13878,#13879,#13880,
#13881,#13882,#13883,#13884,#13885,#13886,#13887,#13888,#13889,#13890,#13891,
#13892,#13893,#13894,#13895),.UNSPECIFIED.,.F.,.F.,(4,3,3,3,3,3,3,3,3,3,
4),(-5.63655962566659E-6,0.000138967995190904,0.000300786409144175,0.00041832036912045,
0.00049892390649278,0.000607102001454561,0.000706192477737142,0.000797150254787515,
0.000884559421701961,0.000968128215167521,0.00100346390658489),
 .UNSPECIFIED.);
#149=B_SPLINE_CURVE_WITH_KNOTS('',3,(#13920,#13921,#13922,#13923,#13924,
#13925,#13926,#13927,#13928,#13929,#13930,#13931,#13932,#13933,#13934,#13935,
#13936,#13937,#13938,#13939,#13940,#13941,#13942,#13943,#13944,#13945,#13946,
#13947,#13948,#13949,#13950),.UNSPECIFIED.,.F.,.F.,(4,3,3,3,3,3,3,3,3,3,
4),(2.03723849519033E-8,8.34362343361756E-5,0.000169714572665549,0.000262192396983797,
0.000359257396479951,0.000466160298033514,0.00050278592363799,0.000616382140865371,
0.000756949409341133,0.000924038066230108,0.00100557184727598),
 .UNSPECIFIED.);
#150=B_SPLINE_CURVE_WITH_KNOTS('',3,(#13975,#13976,#13977,#13978,#13979,
#13980,#13981,#13982,#13983,#13984,#13985,#13986,#13987,#13988,#13989,#13990,
#13991,#13992,#13993,#13994,#13995,#13996,#13997,#13998,#13999,#14000,#14001,
#14002,#14003,#14004,#14005),.UNSPECIFIED.,.F.,.F.,(4,3,3,3,3,3,3,3,3,3,
4),(-5.63655962566647E-6,0.000138967995317118,0.00030078640930236,0.000418320369284012,
0.000498923906492781,0.000607102001183047,0.000706192482866764,0.000797150259424217,
0.000884559425945727,0.000968128218988905,0.00100346392791791),
 .UNSPECIFIED.);
#209=(
BOUNDED_CURVE()
B_SPLINE_CURVE(2,(#13443,#13444,#13445),.UNSPECIFIED.,.F.,.F.)
B_SPLINE_CURVE_WITH_KNOTS((3,3),(1.19691741652703,2.09556504436786),
 .UNSPECIFIED.)
CURVE()
GEOMETRIC_REPRESENTATION_ITEM()
RATIONAL_B_SPLINE_CURVE((1.52268468506016,1.64046475534049,1.64046475534049))
REPRESENTATION_ITEM('')
);
#210=(
BOUNDED_CURVE()
B_SPLINE_CURVE(2,(#13446,#13447,#13448),.UNSPECIFIED.,.F.,.F.)
B_SPLINE_CURVE_WITH_KNOTS((3,3),(2.09556504436786,2.9942126722087),
 .UNSPECIFIED.)
CURVE()
GEOMETRIC_REPRESENTATION_ITEM()
RATIONAL_B_SPLINE_CURVE((1.64046475534049,1.64046475534049,1.52268468506016))
REPRESENTATION_ITEM('')
);
#211=(
BOUNDED_CURVE()
B_SPLINE_CURVE(2,(#13491,#13492,#13493),.UNSPECIFIED.,.F.,.F.)
B_SPLINE_CURVE_WITH_KNOTS((3,3),(1.19691741652693,2.09556504436774),
 .UNSPECIFIED.)
CURVE()
GEOMETRIC_REPRESENTATION_ITEM()
RATIONAL_B_SPLINE_CURVE((1.52268468506012,1.64046475534044,1.64046475534044))
REPRESENTATION_ITEM('')
);
#212=(
BOUNDED_CURVE()
B_SPLINE_CURVE(2,(#13494,#13495,#13496),.UNSPECIFIED.,.F.,.F.)
B_SPLINE_CURVE_WITH_KNOTS((3,3),(2.09556504436774,2.99421267220854),
 .UNSPECIFIED.)
CURVE()
GEOMETRIC_REPRESENTATION_ITEM()
RATIONAL_B_SPLINE_CURVE((1.64046475534044,1.64046475534044,1.52268468506012))
REPRESENTATION_ITEM('')
);
#213=(
BOUNDED_CURVE()
B_SPLINE_CURVE(2,(#13539,#13540,#13541),.UNSPECIFIED.,.F.,.F.)
B_SPLINE_CURVE_WITH_KNOTS((3,3),(2.09556504652211,2.99421267491808),
 .UNSPECIFIED.)
CURVE()
GEOMETRIC_REPRESENTATION_ITEM()
RATIONAL_B_SPLINE_CURVE((1.64046475620257,1.64046475620257,1.52268468586035))
REPRESENTATION_ITEM('')
);
#214=(
BOUNDED_CURVE()
B_SPLINE_CURVE(2,(#13542,#13543,#13544),.UNSPECIFIED.,.F.,.F.)
B_SPLINE_CURVE_WITH_KNOTS((3,3),(1.19691741812614,2.09556504652211),
 .UNSPECIFIED.)
CURVE()
GEOMETRIC_REPRESENTATION_ITEM()
RATIONAL_B_SPLINE_CURVE((1.52268468586035,1.64046475620257,1.64046475620257))
REPRESENTATION_ITEM('')
);
#215=(
BOUNDED_CURVE()
B_SPLINE_CURVE(2,(#13587,#13588,#13589),.UNSPECIFIED.,.F.,.F.)
B_SPLINE_CURVE_WITH_KNOTS((3,3),(1.19691741652704,2.09556504436788),
 .UNSPECIFIED.)
CURVE()
GEOMETRIC_REPRESENTATION_ITEM()
RATIONAL_B_SPLINE_CURVE((1.52268468506017,1.6404647553405,1.6404647553405))
REPRESENTATION_ITEM('')
);
#216=(
BOUNDED_CURVE()
B_SPLINE_CURVE(2,(#13590,#13591,#13592),.UNSPECIFIED.,.F.,.F.)
B_SPLINE_CURVE_WITH_KNOTS((3,3),(2.09556504436788,2.99421267220872),
 .UNSPECIFIED.)
CURVE()
GEOMETRIC_REPRESENTATION_ITEM()
RATIONAL_B_SPLINE_CURVE((1.6404647553405,1.6404647553405,1.52268468506017))
REPRESENTATION_ITEM('')
);
#217=(
BOUNDED_CURVE()
B_SPLINE_CURVE(2,(#13635,#13636,#13637),.UNSPECIFIED.,.F.,.F.)
B_SPLINE_CURVE_WITH_KNOTS((3,3),(1.19691741652693,2.09556504436774),
 .UNSPECIFIED.)
CURVE()
GEOMETRIC_REPRESENTATION_ITEM()
RATIONAL_B_SPLINE_CURVE((1.52268468506012,1.64046475534044,1.64046475534044))
REPRESENTATION_ITEM('')
);
#218=(
BOUNDED_CURVE()
B_SPLINE_CURVE(2,(#13638,#13639,#13640),.UNSPECIFIED.,.F.,.F.)
B_SPLINE_CURVE_WITH_KNOTS((3,3),(2.09556504436774,2.99421267220854),
 .UNSPECIFIED.)
CURVE()
GEOMETRIC_REPRESENTATION_ITEM()
RATIONAL_B_SPLINE_CURVE((1.64046475534044,1.64046475534044,1.52268468506012))
REPRESENTATION_ITEM('')
);
#219=(
BOUNDED_CURVE()
B_SPLINE_CURVE(2,(#13680,#13681,#13682),.UNSPECIFIED.,.F.,.F.)
B_SPLINE_CURVE_WITH_KNOTS((3,3),(1.19691742009084,2.09556504916886),
 .UNSPECIFIED.)
CURVE()
GEOMETRIC_REPRESENTATION_ITEM()
RATIONAL_B_SPLINE_CURVE((1.52268468684348,1.64046475726175,1.64046475726175))
REPRESENTATION_ITEM('')
);
#220=(
BOUNDED_CURVE()
B_SPLINE_CURVE(2,(#13683,#13684,#13685),.UNSPECIFIED.,.F.,.F.)
B_SPLINE_CURVE_WITH_KNOTS((3,3),(2.09556504916886,2.99421267824688),
 .UNSPECIFIED.)
CURVE()
GEOMETRIC_REPRESENTATION_ITEM()
RATIONAL_B_SPLINE_CURVE((1.64046475726175,1.64046475726175,1.52268468684348))
REPRESENTATION_ITEM('')
);
#228=SHAPE_REPRESENTATION_RELATIONSHIP('SRR','None',#14127,#237);
#237=ADVANCED_BREP_SHAPE_REPRESENTATION('',(#255),#14082);
#246=STYLED_ITEM('',(#14177),#255);
#255=MANIFOLD_SOLID_BREP('Body1',#3472);
#281=FACE_BOUND('',#749,.T.);
#282=FACE_BOUND('',#751,.T.);
#353=PLANE('',#3820);
#354=PLANE('',#3821);
#355=PLANE('',#3822);
#356=PLANE('',#3823);
#357=PLANE('',#3824);
#358=PLANE('',#3825);
#359=PLANE('',#3826);
#360=PLANE('',#3833);
#522=FACE_OUTER_BOUND('',#736,.T.);
#523=FACE_OUTER_BOUND('',#737,.T.);
#524=FACE_OUTER_BOUND('',#738,.T.);
#525=FACE_OUTER_BOUND('',#739,.T.);
#526=FACE_OUTER_BOUND('',#740,.T.);
#527=FACE_OUTER_BOUND('',#741,.T.);
#528=FACE_OUTER_BOUND('',#742,.T.);
#529=FACE_OUTER_BOUND('',#743,.T.);
#530=FACE_OUTER_BOUND('',#744,.T.);
#531=FACE_OUTER_BOUND('',#745,.T.);
#532=FACE_OUTER_BOUND('',#746,.T.);
#533=FACE_OUTER_BOUND('',#747,.T.);
#534=FACE_OUTER_BOUND('',#748,.T.);
#535=FACE_OUTER_BOUND('',#750,.T.);
#536=FACE_OUTER_BOUND('',#752,.T.);
#537=FACE_OUTER_BOUND('',#753,.T.);
#538=FACE_OUTER_BOUND('',#754,.T.);
#539=FACE_OUTER_BOUND('',#755,.T.);
#540=FACE_OUTER_BOUND('',#756,.T.);
#541=FACE_OUTER_BOUND('',#757,.T.);
#542=FACE_OUTER_BOUND('',#758,.T.);
#543=FACE_OUTER_BOUND('',#759,.T.);
#544=FACE_OUTER_BOUND('',#760,.T.);
#545=FACE_OUTER_BOUND('',#761,.T.);
#546=FACE_OUTER_BOUND('',#762,.T.);
#547=FACE_OUTER_BOUND('',#763,.T.);
#736=EDGE_LOOP('',(#3049,#3050,#3051,#3052,#3053));
#737=EDGE_LOOP('',(#3054,#3055,#3056,#3057,#3058,#3059));
#738=EDGE_LOOP('',(#3060,#3061,#3062,#3063));
#739=EDGE_LOOP('',(#3064,#3065,#3066,#3067,#3068,#3069,#3070,#3071,#3072,
#3073,#3074,#3075));
#740=EDGE_LOOP('',(#3076,#3077,#3078,#3079,#3080));
#741=EDGE_LOOP('',(#3081,#3082,#3083,#3084,#3085));
#742=EDGE_LOOP('',(#3086,#3087,#3088,#3089,#3090));
#743=EDGE_LOOP('',(#3091,#3092,#3093,#3094,#3095));
#744=EDGE_LOOP('',(#3096,#3097,#3098,#3099,#3100));
#745=EDGE_LOOP('',(#3101,#3102,#3103,#3104,#3105));
#746=EDGE_LOOP('',(#3106,#3107,#3108,#3109,#3110));
#747=EDGE_LOOP('',(#3111,#3112,#3113,#3114,#3115));
#748=EDGE_LOOP('',(#3116,#3117,#3118,#3119,#3120,#3121));
#749=EDGE_LOOP('',(#3122));
#750=EDGE_LOOP('',(#3123));
#751=EDGE_LOOP('',(#3124));
#752=EDGE_LOOP('',(#3125,#3126,#3127));
#753=EDGE_LOOP('',(#3128,#3129,#3130));
#754=EDGE_LOOP('',(#3131,#3132,#3133));
#755=EDGE_LOOP('',(#3134,#3135,#3136));
#756=EDGE_LOOP('',(#3137,#3138,#3139));
#757=EDGE_LOOP('',(#3140,#3141,#3142));
#758=EDGE_LOOP('',(#3143,#3144,#3145,#3146));
#759=EDGE_LOOP('',(#3147,#3148,#3149,#3150));
#760=EDGE_LOOP('',(#3151,#3152,#3153,#3154,#3155));
#761=EDGE_LOOP('',(#3156,#3157,#3158,#3159,#3160));
#762=EDGE_LOOP('',(#3161,#3162,#3163,#3164));
#763=EDGE_LOOP('',(#3165,#3166,#3167,#3168));
#1016=LINE('',#13282,#1273);
#1017=LINE('',#13290,#1274);
#1018=LINE('',#13296,#1275);
#1019=LINE('',#13303,#1276);
#1020=LINE('',#13397,#1277);
#1021=LINE('',#13401,#1278);
#1022=LINE('',#13441,#1279);
#1023=LINE('',#13452,#1280);
#1024=LINE('',#13500,#1281);
#1025=LINE('',#13548,#1282);
#1026=LINE('',#13596,#1283);
#1273=VECTOR('',#4569,6.);
#1274=VECTOR('',#4578,6.);
#1275=VECTOR('',#4585,5.01);
#1276=VECTOR('',#4592,12.389406481562);
#1277=VECTOR('',#4603,5.1);
#1278=VECTOR('',#4606,1000.);
#1279=VECTOR('',#4607,1000.);
#1280=VECTOR('',#4610,1000.);
#1281=VECTOR('',#4613,1000.);
#1282=VECTOR('',#4616,1000.);
#1283=VECTOR('',#4619,1000.);
#1354=CIRCLE('',#3804,6.);
#1355=CIRCLE('',#3805,6.);
#1356=CIRCLE('',#3806,6.);
#1357=CIRCLE('',#3808,5.1);
#1358=CIRCLE('',#3809,5.1);
#1359=CIRCLE('',#3811,5.1);
#1360=CIRCLE('',#3812,6.);
#1361=CIRCLE('',#3814,12.389406481562);
#1362=CIRCLE('',#3815,12.389406481562);
#1363=CIRCLE('',#3817,0.927982083713184);
#1364=CIRCLE('',#3818,12.0720179162868);
#1365=CIRCLE('',#3827,9.);
#1366=CIRCLE('',#3828,9.);
#1367=CIRCLE('',#3829,9.);
#1368=CIRCLE('',#3830,9.);
#1369=CIRCLE('',#3831,9.);
#1370=CIRCLE('',#3832,9.);
#1660=VERTEX_POINT('',#13279);
#1661=VERTEX_POINT('',#13281);
#1662=VERTEX_POINT('',#13283);
#1663=VERTEX_POINT('',#13287);
#1664=VERTEX_POINT('',#13288);
#1665=VERTEX_POINT('',#13293);
#1666=VERTEX_POINT('',#13295);
#1667=VERTEX_POINT('',#13299);
#1668=VERTEX_POINT('',#13300);
#1669=VERTEX_POINT('',#13302);
#1670=VERTEX_POINT('',#13304);
#1671=VERTEX_POINT('',#13311);
#1672=VERTEX_POINT('',#13322);
#1673=VERTEX_POINT('',#13333);
#1674=VERTEX_POINT('',#13356);
#1675=VERTEX_POINT('',#13363);
#1676=VERTEX_POINT('',#13374);
#1677=VERTEX_POINT('',#13393);
#1678=VERTEX_POINT('',#13399);
#1679=VERTEX_POINT('',#13400);
#1680=VERTEX_POINT('',#13402);
#1681=VERTEX_POINT('',#13440);
#1682=VERTEX_POINT('',#13442);
#1683=VERTEX_POINT('',#13450);
#1684=VERTEX_POINT('',#13451);
#1685=VERTEX_POINT('',#13490);
#1686=VERTEX_POINT('',#13498);
#1687=VERTEX_POINT('',#13499);
#1688=VERTEX_POINT('',#13538);
#1689=VERTEX_POINT('',#13546);
#1690=VERTEX_POINT('',#13547);
#1691=VERTEX_POINT('',#13586);
#1692=VERTEX_POINT('',#13594);
#1693=VERTEX_POINT('',#13595);
#1694=VERTEX_POINT('',#13634);
#1695=VERTEX_POINT('',#13679);
#2128=EDGE_CURVE('',#1660,#1660,#1354,.T.);
#2129=EDGE_CURVE('',#1660,#1661,#1016,.T.);
#2130=EDGE_CURVE('',#1661,#1662,#1355,.T.);
#2131=EDGE_CURVE('',#1662,#1661,#1356,.T.);
#2132=EDGE_CURVE('',#1663,#1664,#1357,.T.);
#2133=EDGE_CURVE('',#1664,#1662,#1017,.T.);
#2134=EDGE_CURVE('',#1664,#1663,#1358,.T.);
#2135=EDGE_CURVE('',#1665,#1665,#1359,.T.);
#2136=EDGE_CURVE('',#1665,#1666,#1018,.T.);
#2137=EDGE_CURVE('',#1666,#1666,#1360,.T.);
#2138=EDGE_CURVE('',#1667,#1668,#1361,.T.);
#2139=EDGE_CURVE('',#1668,#1669,#1019,.T.);
#2140=EDGE_CURVE('',#1669,#1670,#131,.T.);
#2141=EDGE_CURVE('',#1670,#1671,#132,.T.);
#2142=EDGE_CURVE('',#1671,#1672,#133,.T.);
#2143=EDGE_CURVE('',#1672,#1673,#134,.T.);
#2144=EDGE_CURVE('',#1673,#1674,#135,.T.);
#2145=EDGE_CURVE('',#1674,#1675,#136,.T.);
#2146=EDGE_CURVE('',#1675,#1676,#137,.T.);
#2147=EDGE_CURVE('',#1676,#1669,#138,.T.);
#2148=EDGE_CURVE('',#1668,#1667,#1362,.T.);
#2149=EDGE_CURVE('',#1667,#1677,#1363,.T.);
#2150=EDGE_CURVE('',#1677,#1677,#1364,.T.);
#2151=EDGE_CURVE('',#1663,#1665,#1020,.T.);
#2152=EDGE_CURVE('',#1678,#1679,#1021,.T.);
#2153=EDGE_CURVE('',#1678,#1680,#139,.T.);
#2154=EDGE_CURVE('',#1680,#1681,#1022,.T.);
#2155=EDGE_CURVE('',#1681,#1682,#209,.T.);
#2156=EDGE_CURVE('',#1682,#1679,#210,.T.);
#2157=EDGE_CURVE('',#1683,#1684,#1023,.T.);
#2158=EDGE_CURVE('',#1683,#1678,#140,.T.);
#2159=EDGE_CURVE('',#1679,#1685,#211,.T.);
#2160=EDGE_CURVE('',#1685,#1684,#212,.T.);
#2161=EDGE_CURVE('',#1686,#1687,#1024,.T.);
#2162=EDGE_CURVE('',#1686,#1683,#141,.T.);
#2163=EDGE_CURVE('',#1688,#1684,#213,.T.);
#2164=EDGE_CURVE('',#1687,#1688,#214,.T.);
#2165=EDGE_CURVE('',#1689,#1690,#1025,.T.);
#2166=EDGE_CURVE('',#1689,#1686,#142,.T.);
#2167=EDGE_CURVE('',#1687,#1691,#215,.T.);
#2168=EDGE_CURVE('',#1691,#1690,#216,.T.);
#2169=EDGE_CURVE('',#1692,#1693,#1026,.T.);
#2170=EDGE_CURVE('',#1692,#1689,#143,.T.);
#2171=EDGE_CURVE('',#1690,#1694,#217,.T.);
#2172=EDGE_CURVE('',#1694,#1693,#218,.T.);
#2173=EDGE_CURVE('',#1680,#1692,#144,.T.);
#2174=EDGE_CURVE('',#1693,#1695,#219,.T.);
#2175=EDGE_CURVE('',#1695,#1681,#220,.T.);
#2176=EDGE_CURVE('',#1691,#1688,#1365,.T.);
#2177=EDGE_CURVE('',#1688,#1685,#1366,.T.);
#2178=EDGE_CURVE('',#1685,#1682,#1367,.T.);
#2179=EDGE_CURVE('',#1682,#1695,#1368,.T.);
#2180=EDGE_CURVE('',#1695,#1694,#1369,.T.);
#2181=EDGE_CURVE('',#1694,#1691,#1370,.T.);
#2182=EDGE_CURVE('',#1672,#1692,#145,.T.);
#2183=EDGE_CURVE('',#1689,#1671,#146,.T.);
#2184=EDGE_CURVE('',#1686,#1670,#147,.T.);
#2185=EDGE_CURVE('',#1674,#1680,#148,.T.);
#2186=EDGE_CURVE('',#1683,#1676,#149,.T.);
#2187=EDGE_CURVE('',#1675,#1678,#150,.T.);
#3049=ORIENTED_EDGE('',*,*,#2128,.T.);
#3050=ORIENTED_EDGE('',*,*,#2129,.T.);
#3051=ORIENTED_EDGE('',*,*,#2130,.T.);
#3052=ORIENTED_EDGE('',*,*,#2131,.T.);
#3053=ORIENTED_EDGE('',*,*,#2129,.F.);
#3054=ORIENTED_EDGE('',*,*,#2132,.T.);
#3055=ORIENTED_EDGE('',*,*,#2133,.T.);
#3056=ORIENTED_EDGE('',*,*,#2130,.F.);
#3057=ORIENTED_EDGE('',*,*,#2131,.F.);
#3058=ORIENTED_EDGE('',*,*,#2133,.F.);
#3059=ORIENTED_EDGE('',*,*,#2134,.T.);
#3060=ORIENTED_EDGE('',*,*,#2135,.T.);
#3061=ORIENTED_EDGE('',*,*,#2136,.T.);
#3062=ORIENTED_EDGE('',*,*,#2137,.T.);
#3063=ORIENTED_EDGE('',*,*,#2136,.F.);
#3064=ORIENTED_EDGE('',*,*,#2138,.T.);
#3065=ORIENTED_EDGE('',*,*,#2139,.T.);
#3066=ORIENTED_EDGE('',*,*,#2140,.T.);
#3067=ORIENTED_EDGE('',*,*,#2141,.T.);
#3068=ORIENTED_EDGE('',*,*,#2142,.T.);
#3069=ORIENTED_EDGE('',*,*,#2143,.T.);
#3070=ORIENTED_EDGE('',*,*,#2144,.T.);
#3071=ORIENTED_EDGE('',*,*,#2145,.T.);
#3072=ORIENTED_EDGE('',*,*,#2146,.T.);
#3073=ORIENTED_EDGE('',*,*,#2147,.T.);
#3074=ORIENTED_EDGE('',*,*,#2139,.F.);
#3075=ORIENTED_EDGE('',*,*,#2148,.T.);
#3076=ORIENTED_EDGE('',*,*,#2138,.F.);
#3077=ORIENTED_EDGE('',*,*,#2149,.T.);
#3078=ORIENTED_EDGE('',*,*,#2150,.T.);
#3079=ORIENTED_EDGE('',*,*,#2149,.F.);
#3080=ORIENTED_EDGE('',*,*,#2148,.F.);
#3081=ORIENTED_EDGE('',*,*,#2132,.F.);
#3082=ORIENTED_EDGE('',*,*,#2151,.T.);
#3083=ORIENTED_EDGE('',*,*,#2135,.F.);
#3084=ORIENTED_EDGE('',*,*,#2151,.F.);
#3085=ORIENTED_EDGE('',*,*,#2134,.F.);
#3086=ORIENTED_EDGE('',*,*,#2152,.F.);
#3087=ORIENTED_EDGE('',*,*,#2153,.T.);
#3088=ORIENTED_EDGE('',*,*,#2154,.T.);
#3089=ORIENTED_EDGE('',*,*,#2155,.T.);
#3090=ORIENTED_EDGE('',*,*,#2156,.T.);
#3091=ORIENTED_EDGE('',*,*,#2157,.F.);
#3092=ORIENTED_EDGE('',*,*,#2158,.T.);
#3093=ORIENTED_EDGE('',*,*,#2152,.T.);
#3094=ORIENTED_EDGE('',*,*,#2159,.T.);
#3095=ORIENTED_EDGE('',*,*,#2160,.T.);
#3096=ORIENTED_EDGE('',*,*,#2161,.F.);
#3097=ORIENTED_EDGE('',*,*,#2162,.T.);
#3098=ORIENTED_EDGE('',*,*,#2157,.T.);
#3099=ORIENTED_EDGE('',*,*,#2163,.F.);
#3100=ORIENTED_EDGE('',*,*,#2164,.F.);
#3101=ORIENTED_EDGE('',*,*,#2165,.F.);
#3102=ORIENTED_EDGE('',*,*,#2166,.T.);
#3103=ORIENTED_EDGE('',*,*,#2161,.T.);
#3104=ORIENTED_EDGE('',*,*,#2167,.T.);
#3105=ORIENTED_EDGE('',*,*,#2168,.T.);
#3106=ORIENTED_EDGE('',*,*,#2169,.F.);
#3107=ORIENTED_EDGE('',*,*,#2170,.T.);
#3108=ORIENTED_EDGE('',*,*,#2165,.T.);
#3109=ORIENTED_EDGE('',*,*,#2171,.T.);
#3110=ORIENTED_EDGE('',*,*,#2172,.T.);
#3111=ORIENTED_EDGE('',*,*,#2154,.F.);
#3112=ORIENTED_EDGE('',*,*,#2173,.T.);
#3113=ORIENTED_EDGE('',*,*,#2169,.T.);
#3114=ORIENTED_EDGE('',*,*,#2174,.T.);
#3115=ORIENTED_EDGE('',*,*,#2175,.T.);
#3116=ORIENTED_EDGE('',*,*,#2176,.T.);
#3117=ORIENTED_EDGE('',*,*,#2177,.T.);
#3118=ORIENTED_EDGE('',*,*,#2178,.T.);
#3119=ORIENTED_EDGE('',*,*,#2179,.T.);
#3120=ORIENTED_EDGE('',*,*,#2180,.T.);
#3121=ORIENTED_EDGE('',*,*,#2181,.T.);
#3122=ORIENTED_EDGE('',*,*,#2137,.F.);
#3123=ORIENTED_EDGE('',*,*,#2150,.F.);
#3124=ORIENTED_EDGE('',*,*,#2128,.F.);
#3125=ORIENTED_EDGE('',*,*,#2164,.T.);
#3126=ORIENTED_EDGE('',*,*,#2176,.F.);
#3127=ORIENTED_EDGE('',*,*,#2167,.F.);
#3128=ORIENTED_EDGE('',*,*,#2181,.F.);
#3129=ORIENTED_EDGE('',*,*,#2171,.F.);
#3130=ORIENTED_EDGE('',*,*,#2168,.F.);
#3131=ORIENTED_EDGE('',*,*,#2180,.F.);
#3132=ORIENTED_EDGE('',*,*,#2174,.F.);
#3133=ORIENTED_EDGE('',*,*,#2172,.F.);
#3134=ORIENTED_EDGE('',*,*,#2175,.F.);
#3135=ORIENTED_EDGE('',*,*,#2179,.F.);
#3136=ORIENTED_EDGE('',*,*,#2155,.F.);
#3137=ORIENTED_EDGE('',*,*,#2178,.F.);
#3138=ORIENTED_EDGE('',*,*,#2159,.F.);
#3139=ORIENTED_EDGE('',*,*,#2156,.F.);
#3140=ORIENTED_EDGE('',*,*,#2177,.F.);
#3141=ORIENTED_EDGE('',*,*,#2163,.T.);
#3142=ORIENTED_EDGE('',*,*,#2160,.F.);
#3143=ORIENTED_EDGE('',*,*,#2182,.F.);
#3144=ORIENTED_EDGE('',*,*,#2142,.F.);
#3145=ORIENTED_EDGE('',*,*,#2183,.F.);
#3146=ORIENTED_EDGE('',*,*,#2170,.F.);
#3147=ORIENTED_EDGE('',*,*,#2183,.T.);
#3148=ORIENTED_EDGE('',*,*,#2141,.F.);
#3149=ORIENTED_EDGE('',*,*,#2184,.F.);
#3150=ORIENTED_EDGE('',*,*,#2166,.F.);
#3151=ORIENTED_EDGE('',*,*,#2182,.T.);
#3152=ORIENTED_EDGE('',*,*,#2173,.F.);
#3153=ORIENTED_EDGE('',*,*,#2185,.F.);
#3154=ORIENTED_EDGE('',*,*,#2144,.F.);
#3155=ORIENTED_EDGE('',*,*,#2143,.F.);
#3156=ORIENTED_EDGE('',*,*,#2184,.T.);
#3157=ORIENTED_EDGE('',*,*,#2140,.F.);
#3158=ORIENTED_EDGE('',*,*,#2147,.F.);
#3159=ORIENTED_EDGE('',*,*,#2186,.F.);
#3160=ORIENTED_EDGE('',*,*,#2162,.F.);
#3161=ORIENTED_EDGE('',*,*,#2185,.T.);
#3162=ORIENTED_EDGE('',*,*,#2153,.F.);
#3163=ORIENTED_EDGE('',*,*,#2187,.F.);
#3164=ORIENTED_EDGE('',*,*,#2145,.F.);
#3165=ORIENTED_EDGE('',*,*,#2186,.T.);
#3166=ORIENTED_EDGE('',*,*,#2146,.F.);
#3167=ORIENTED_EDGE('',*,*,#2187,.T.);
#3168=ORIENTED_EDGE('',*,*,#2158,.F.);
#3270=CYLINDRICAL_SURFACE('',#3803,6.);
#3271=CYLINDRICAL_SURFACE('',#3819,5.1);
#3432=ADVANCED_FACE('',(#522),#3270,.F.);
#3433=ADVANCED_FACE('',(#523),#52,.F.);
#3434=ADVANCED_FACE('',(#524),#53,.F.);
#3435=ADVANCED_FACE('',(#525),#54,.T.);
#3436=ADVANCED_FACE('',(#526),#72,.T.);
#3437=ADVANCED_FACE('',(#527),#3271,.F.);
#3438=ADVANCED_FACE('',(#528),#353,.T.);
#3439=ADVANCED_FACE('',(#529),#354,.T.);
#3440=ADVANCED_FACE('',(#530),#355,.F.);
#3441=ADVANCED_FACE('',(#531),#356,.T.);
#3442=ADVANCED_FACE('',(#532),#357,.T.);
#3443=ADVANCED_FACE('',(#533),#358,.T.);
#3444=ADVANCED_FACE('',(#534,#281),#359,.T.);
#3445=ADVANCED_FACE('',(#535,#282),#360,.F.);
#3446=ADVANCED_FACE('',(#536),#55,.T.);
#3447=ADVANCED_FACE('',(#537),#56,.T.);
#3448=ADVANCED_FACE('',(#538),#57,.T.);
#3449=ADVANCED_FACE('',(#539),#58,.T.);
#3450=ADVANCED_FACE('',(#540),#59,.T.);
#3451=ADVANCED_FACE('',(#541),#60,.T.);
#3452=ADVANCED_FACE('',(#542),#65,.F.);
#3453=ADVANCED_FACE('',(#543),#66,.F.);
#3454=ADVANCED_FACE('',(#544),#67,.F.);
#3455=ADVANCED_FACE('',(#545),#68,.F.);
#3456=ADVANCED_FACE('',(#546),#69,.F.);
#3457=ADVANCED_FACE('',(#547),#70,.F.);
#3472=CLOSED_SHELL('',(#3432,#3433,#3434,#3435,#3436,#3437,#3438,#3439,
#3440,#3441,#3442,#3443,#3444,#3445,#3446,#3447,#3448,#3449,#3450,#3451,
#3452,#3453,#3454,#3455,#3456,#3457));
#3802=AXIS2_PLACEMENT_3D('',#13277,#4563,#4564);
#3803=AXIS2_PLACEMENT_3D('',#13278,#4565,#4566);
#3804=AXIS2_PLACEMENT_3D('',#13280,#4567,#4568);
#3805=AXIS2_PLACEMENT_3D('',#13284,#4570,#4571);
#3806=AXIS2_PLACEMENT_3D('',#13285,#4572,#4573);
#3807=AXIS2_PLACEMENT_3D('',#13286,#4574,#4575);
#3808=AXIS2_PLACEMENT_3D('',#13289,#4576,#4577);
#3809=AXIS2_PLACEMENT_3D('',#13291,#4579,#4580);
#3810=AXIS2_PLACEMENT_3D('',#13292,#4581,#4582);
#3811=AXIS2_PLACEMENT_3D('',#13294,#4583,#4584);
#3812=AXIS2_PLACEMENT_3D('',#13297,#4586,#4587);
#3813=AXIS2_PLACEMENT_3D('',#13298,#4588,#4589);
#3814=AXIS2_PLACEMENT_3D('',#13301,#4590,#4591);
#3815=AXIS2_PLACEMENT_3D('',#13391,#4593,#4594);
#3816=AXIS2_PLACEMENT_3D('',#13392,#4595,#4596);
#3817=AXIS2_PLACEMENT_3D('',#13394,#4597,#4598);
#3818=AXIS2_PLACEMENT_3D('',#13395,#4599,#4600);
#3819=AXIS2_PLACEMENT_3D('',#13396,#4601,#4602);
#3820=AXIS2_PLACEMENT_3D('',#13398,#4604,#4605);
#3821=AXIS2_PLACEMENT_3D('',#13449,#4608,#4609);
#3822=AXIS2_PLACEMENT_3D('',#13497,#4611,#4612);
#3823=AXIS2_PLACEMENT_3D('',#13545,#4614,#4615);
#3824=AXIS2_PLACEMENT_3D('',#13593,#4617,#4618);
#3825=AXIS2_PLACEMENT_3D('',#13641,#4620,#4621);
#3826=AXIS2_PLACEMENT_3D('',#13686,#4622,#4623);
#3827=AXIS2_PLACEMENT_3D('',#13687,#4624,#4625);
#3828=AXIS2_PLACEMENT_3D('',#13688,#4626,#4627);
#3829=AXIS2_PLACEMENT_3D('',#13689,#4628,#4629);
#3830=AXIS2_PLACEMENT_3D('',#13690,#4630,#4631);
#3831=AXIS2_PLACEMENT_3D('',#13691,#4632,#4633);
#3832=AXIS2_PLACEMENT_3D('',#13692,#4634,#4635);
#3833=AXIS2_PLACEMENT_3D('',#13693,#4636,#4637);
#3834=AXIS2_PLACEMENT_3D('',#13694,#4638,#4639);
#3835=AXIS2_PLACEMENT_3D('',#13695,#4640,#4641);
#3836=AXIS2_PLACEMENT_3D('',#13696,#4642,#4643);
#3837=AXIS2_PLACEMENT_3D('',#13697,#4644,#4645);
#3838=AXIS2_PLACEMENT_3D('',#13698,#4646,#4647);
#3839=AXIS2_PLACEMENT_3D('',#13699,#4648,#4649);
#4563=DIRECTION('axis',(0.,0.,1.));
#4564=DIRECTION('refdir',(1.,0.,0.));
#4565=DIRECTION('center_axis',(0.,0.,1.));
#4566=DIRECTION('ref_axis',(1.,0.,0.));
#4567=DIRECTION('center_axis',(0.,0.,-1.));
#4568=DIRECTION('ref_axis',(1.,0.,0.));
#4569=DIRECTION('',(0.,0.,1.));
#4570=DIRECTION('center_axis',(0.,0.,1.));
#4571=DIRECTION('ref_axis',(1.,0.,0.));
#4572=DIRECTION('center_axis',(0.,0.,1.));
#4573=DIRECTION('ref_axis',(1.,0.,0.));
#4574=DIRECTION('center_axis',(0.,0.,-1.));
#4575=DIRECTION('ref_axis',(-1.,0.,0.));
#4576=DIRECTION('center_axis',(0.,0.,1.));
#4577=DIRECTION('ref_axis',(-1.,0.,0.));
#4578=DIRECTION('',(0.81915204428899,-1.00317192905352E-16,-0.573576436351048));
#4579=DIRECTION('center_axis',(0.,0.,1.));
#4580=DIRECTION('ref_axis',(-1.,0.,0.));
#4581=DIRECTION('center_axis',(0.,0.,1.));
#4582=DIRECTION('ref_axis',(1.,0.,0.));
#4583=DIRECTION('center_axis',(0.,0.,-1.));
#4584=DIRECTION('ref_axis',(1.,0.,0.));
#4585=DIRECTION('',(-0.819152044288991,-1.00317192905352E-16,0.573576436351046));
#4586=DIRECTION('center_axis',(0.,0.,1.));
#4587=DIRECTION('ref_axis',(1.,0.,0.));
#4588=DIRECTION('center_axis',(0.,0.,-1.));
#4589=DIRECTION('ref_axis',(-1.,0.,0.));
#4590=DIRECTION('center_axis',(0.,0.,1.));
#4591=DIRECTION('ref_axis',(1.,0.,0.));
#4592=DIRECTION('',(-0.939692620785915,1.15079156022786E-16,0.342020143325652));
#4593=DIRECTION('center_axis',(0.,0.,1.));
#4594=DIRECTION('ref_axis',(1.,0.,0.));
#4595=DIRECTION('center_axis',(0.,0.,1.));
#4596=DIRECTION('ref_axis',(1.,0.,0.));
#4597=DIRECTION('center_axis',(1.22464679914735E-16,-1.,0.));
#4598=DIRECTION('ref_axis',(-1.,-1.22464679914735E-16,0.));
#4599=DIRECTION('center_axis',(0.,0.,1.));
#4600=DIRECTION('ref_axis',(1.,0.,0.));
#4601=DIRECTION('center_axis',(0.,0.,1.));
#4602=DIRECTION('ref_axis',(1.,0.,0.));
#4603=DIRECTION('',(0.,0.,1.));
#4604=DIRECTION('center_axis',(-0.5,0.866025403784438,0.));
#4605=DIRECTION('ref_axis',(-0.866025403784438,-0.5,0.));
#4606=DIRECTION('',(0.,0.,1.));
#4607=DIRECTION('',(0.,0.,1.));
#4608=DIRECTION('center_axis',(0.5,0.866025403784438,0.));
#4609=DIRECTION('ref_axis',(-0.866025403784438,0.5,0.));
#4610=DIRECTION('',(0.,0.,1.));
#4611=DIRECTION('center_axis',(-1.,0.,0.));
#4612=DIRECTION('ref_axis',(0.,0.,1.));
#4613=DIRECTION('',(0.,0.,1.));
#4614=DIRECTION('center_axis',(0.5,-0.866025403784438,0.));
#4615=DIRECTION('ref_axis',(0.866025403784438,0.5,0.));
#4616=DIRECTION('',(0.,0.,1.));
#4617=DIRECTION('center_axis',(-0.5,-0.866025403784438,0.));
#4618=DIRECTION('ref_axis',(0.866025403784438,-0.5,0.));
#4619=DIRECTION('',(0.,0.,1.));
#4620=DIRECTION('center_axis',(-1.,0.,0.));
#4621=DIRECTION('ref_axis',(0.,0.,1.));
#4622=DIRECTION('center_axis',(0.,0.,1.));
#4623=DIRECTION('ref_axis',(1.,0.,0.));
#4624=DIRECTION('center_axis',(0.,0.,1.));
#4625=DIRECTION('ref_axis',(1.,0.,0.));
#4626=DIRECTION('center_axis',(0.,0.,1.));
#4627=DIRECTION('ref_axis',(1.,0.,0.));
#4628=DIRECTION('center_axis',(0.,0.,1.));
#4629=DIRECTION('ref_axis',(1.,0.,0.));
#4630=DIRECTION('center_axis',(0.,0.,1.));
#4631=DIRECTION('ref_axis',(1.,0.,0.));
#4632=DIRECTION('center_axis',(0.,0.,1.));
#4633=DIRECTION('ref_axis',(1.,0.,0.));
#4634=DIRECTION('center_axis',(0.,0.,1.));
#4635=DIRECTION('ref_axis',(1.,0.,0.));
#4636=DIRECTION('center_axis',(0.,0.,1.));
#4637=DIRECTION('ref_axis',(1.,0.,0.));
#4638=DIRECTION('center_axis',(0.,0.,-1.));
#4639=DIRECTION('ref_axis',(-1.,0.,0.));
#4640=DIRECTION('center_axis',(0.,0.,-1.));
#4641=DIRECTION('ref_axis',(-1.,0.,0.));
#4642=DIRECTION('center_axis',(0.,0.,-1.));
#4643=DIRECTION('ref_axis',(-1.,0.,0.));
#4644=DIRECTION('center_axis',(0.,0.,-1.));
#4645=DIRECTION('ref_axis',(-1.,0.,0.));
#4646=DIRECTION('center_axis',(0.,0.,-1.));
#4647=DIRECTION('ref_axis',(-1.,0.,0.));
#4648=DIRECTION('center_axis',(0.,0.,-1.));
#4649=DIRECTION('ref_axis',(-1.,0.,0.));
#13277=CARTESIAN_POINT('',(0.,0.,0.));
#13278=CARTESIAN_POINT('Origin',(0.,0.,-25.0375057290932));
#13279=CARTESIAN_POINT('',(-6.,-7.34788079488412E-16,-12.));
#13280=CARTESIAN_POINT('Origin',(0.,0.,-12.));
#13281=CARTESIAN_POINT('',(-6.,-7.34788079488412E-16,-11.9746));
#13282=CARTESIAN_POINT('',(-6.,-7.34788079488412E-16,-25.0375057290932));
#13283=CARTESIAN_POINT('',(6.,7.34788079488412E-16,-11.9746));
#13284=CARTESIAN_POINT('Origin',(0.,0.,-11.9746));
#13285=CARTESIAN_POINT('Origin',(0.,0.,-11.9746));
#13286=CARTESIAN_POINT('Origin',(0.,0.,-11.9746));
#13287=CARTESIAN_POINT('',(-5.1,6.2456986756515E-16,-11.3444132156113));
#13288=CARTESIAN_POINT('',(5.1,-6.2456986756515E-16,-11.3444132156113));
#13289=CARTESIAN_POINT('Origin',(0.,0.,-11.3444132156113));
#13290=CARTESIAN_POINT('',(6.,-7.34788079488412E-16,-11.9746));
#13291=CARTESIAN_POINT('Origin',(0.,0.,-11.3444132156113));
#13292=CARTESIAN_POINT('Origin',(0.,0.,-0.693205462827612));
#13293=CARTESIAN_POINT('',(-5.1,-6.2456986756515E-16,-0.63018678438874));
#13294=CARTESIAN_POINT('Origin',(0.,0.,-0.63018678438874));
#13295=CARTESIAN_POINT('',(-6.,-7.34788079488412E-16,8.32667268468867E-16));
#13296=CARTESIAN_POINT('',(-5.01,-6.13548046372824E-16,-0.693205462827612));
#13297=CARTESIAN_POINT('Origin',(0.,0.,0.));
#13298=CARTESIAN_POINT('Origin',(0.,0.,-10.2));
#13299=CARTESIAN_POINT('',(-12.389406481562,1.51726469909804E-15,-10.2));
#13300=CARTESIAN_POINT('',(12.389406481562,-1.51726469909804E-15,-10.2));
#13301=CARTESIAN_POINT('Origin',(0.,0.,-10.2));
#13302=CARTESIAN_POINT('',(9.47374549680553,1.47832800417317E-13,-9.13878618833741));
#13303=CARTESIAN_POINT('',(12.389406481562,-1.51726469909804E-15,-10.2));
#13304=CARTESIAN_POINT('',(9.50673733309445,-5.48871731080218,-9.68608426626664));
#13305=CARTESIAN_POINT('Ctrl Pts',(9.47374549680553,1.47832800417317E-13,
-9.13878618833741));
#13306=CARTESIAN_POINT('Ctrl Pts',(9.47374549680553,-0.917652977016494,
-9.1387861883374));
#13307=CARTESIAN_POINT('Ctrl Pts',(9.47742023919566,-1.84007744032089,-9.18998243378686));
#13308=CARTESIAN_POINT('Ctrl Pts',(9.48963681266947,-3.67190976040601,-9.38031285482134));
#13309=CARTESIAN_POINT('Ctrl Pts',(9.4979812322815,-4.58224166307851,-9.51835923202207));
#13310=CARTESIAN_POINT('Ctrl Pts',(9.50673734385392,-5.48871730453454,-9.6860842995786));
#13311=CARTESIAN_POINT('',(4.12011128382577E-8,-10.9774346929668,-9.68608426626665));
#13312=CARTESIAN_POINT('Ctrl Pts',(9.50673734443727,-5.48871736492593,-9.68608431075281));
#13313=CARTESIAN_POINT('Ctrl Pts',(8.71694238599845,-5.93459006657547,-9.51827723663476));
#13314=CARTESIAN_POINT('Ctrl Pts',(7.92188072226173,-6.38395964915516,-9.37991057108433));
#13315=CARTESIAN_POINT('Ctrl Pts',(6.33211805884209,-7.28773429047636,-9.19002022026341));
#13316=CARTESIAN_POINT('Ctrl Pts',(5.53677988505539,-7.74269267835578,-9.13897293541538));
#13317=CARTESIAN_POINT('Ctrl Pts',(3.94587469694457,-8.66117228117377,-9.13860048412926));
#13318=CARTESIAN_POINT('Ctrl Pts',(3.14812015320142,-9.12599280095263,-9.18970703534583));
#13319=CARTESIAN_POINT('Ctrl Pts',(1.56631645695501,-10.0533574210071,-9.3800550537477));
#13320=CARTESIAN_POINT('Ctrl Pts',(0.781382220745076,-10.5161833614735,
-9.51820254214856));
#13321=CARTESIAN_POINT('Ctrl Pts',(5.20087756022726E-8,-10.977434699151,
-9.68608429957861));
#13322=CARTESIAN_POINT('',(-9.5067372624267,-5.48871738635801,-9.68608422686381));
#13323=CARTESIAN_POINT('Ctrl Pts',(-8.03821811192016E-16,-10.9774347298519,
-9.68608431075282));
#13324=CARTESIAN_POINT('Ctrl Pts',(-0.781034565701908,-10.5163885828877,
-9.51827723663477));
#13325=CARTESIAN_POINT('Ctrl Pts',(-1.56773087177229,-10.0525297758065,
-9.37991057108433));
#13326=CARTESIAN_POINT('Ctrl Pts',(-3.14530400216244,-9.12764224395764,
-9.19002022026341));
#13327=CARTESIAN_POINT('Ctrl Pts',(-3.93697861062418,-8.66633837479854,
-9.13897293541538));
#13328=CARTESIAN_POINT('Ctrl Pts',(-5.52785787357781,-7.74781386829111,
-9.13860048412926));
#13329=CARTESIAN_POINT('Ctrl Pts',(-6.32928152377817,-7.28934842731451,
-9.18970703534583));
#13330=CARTESIAN_POINT('Ctrl Pts',(-7.92330469143949,-6.38314855259225,
-9.3800550537477));
#13331=CARTESIAN_POINT('Ctrl Pts',(-8.71659083151876,-5.9347885339675,-9.51820254214855));
#13332=CARTESIAN_POINT('Ctrl Pts',(-9.50673726236548,-5.48871741125893,
-9.68608429331509));
#13333=CARTESIAN_POINT('',(-9.47374541791149,5.30814753102003E-12,-9.13878640509698));
#13334=CARTESIAN_POINT('Ctrl Pts',(-9.5067372390073,-5.48871738714607,-9.68608418865576));
#13335=CARTESIAN_POINT('Ctrl Pts',(-9.50309533650332,-5.11181152183886,
-9.6163439615158));
#13336=CARTESIAN_POINT('Ctrl Pts',(-9.49952212465081,-4.73381646984127,
-9.5516635885274));
#13337=CARTESIAN_POINT('Ctrl Pts',(-9.49615224616066,-4.35510455307548,
-9.49309058903634));
#13338=CARTESIAN_POINT('Ctrl Pts',(-9.49313748707562,-4.01630147901212,
-9.44069004021243));
#13339=CARTESIAN_POINT('Ctrl Pts',(-9.49028561895122,-3.67692448753277,
-9.39317786501973));
#13340=CARTESIAN_POINT('Ctrl Pts',(-9.4876923009373,-3.33724242242393,-9.35126210844157));
#13341=CARTESIAN_POINT('Ctrl Pts',(-9.48625162146954,-3.1485370750109,-9.32797642980373));
#13342=CARTESIAN_POINT('Ctrl Pts',(-9.48489070945183,-2.95973763194223,
-9.30641711252709));
#13343=CARTESIAN_POINT('Ctrl Pts',(-9.48362561485523,-2.7708908093873,-9.28669845387052));
#13344=CARTESIAN_POINT('Ctrl Pts',(-9.4835827150424,-2.76448694570475,-9.28602978706251));
#13345=CARTESIAN_POINT('Ctrl Pts',(-9.48353993380462,-2.75808300240005,
-9.28536326917743));
#13346=CARTESIAN_POINT('Ctrl Pts',(-9.48349727158409,-2.75167898135504,
-9.28469890294303));
#13347=CARTESIAN_POINT('Ctrl Pts',(-9.48060306269765,-2.31722961643964,
-9.23962823771928));
#13348=CARTESIAN_POINT('Ctrl Pts',(-9.47825591393638,-1.88234724206654,
-9.20445631983736));
#13349=CARTESIAN_POINT('Ctrl Pts',(-9.47659088198413,-1.44699337073343,
-9.1799546918354));
#13350=CARTESIAN_POINT('Ctrl Pts',(-9.47498141340749,-1.02616758736896,
-9.15627070169182));
#13351=CARTESIAN_POINT('Ctrl Pts',(-9.47400932607905,-0.604901178862813,
-9.14255687393668));
#13352=CARTESIAN_POINT('Ctrl Pts',(-9.47379196605356,-0.183167756031004,
-9.13946164875121));
#13353=CARTESIAN_POINT('Ctrl Pts',(-9.47376050307898,-0.122121627911641,
-9.13901361332646));
#13354=CARTESIAN_POINT('Ctrl Pts',(-9.47374484508027,-0.0610657303984304,
-9.13878797893779));
#13355=CARTESIAN_POINT('Ctrl Pts',(-9.47374533901746,1.0764238021782E-11,
-9.13878662185656));
#13356=CARTESIAN_POINT('',(-9.50673733309446,5.48871731080218,-9.68608426626664));
#13357=CARTESIAN_POINT('Ctrl Pts',(-9.47374549680553,-1.47873570794491E-13,
-9.13878618833741));
#13358=CARTESIAN_POINT('Ctrl Pts',(-9.47374549680553,0.917652977016494,
-9.1387861883374));
#13359=CARTESIAN_POINT('Ctrl Pts',(-9.47742023919566,1.84007744032089,-9.18998243378686));
#13360=CARTESIAN_POINT('Ctrl Pts',(-9.48963681266947,3.67190976040601,-9.38031285482134));
#13361=CARTESIAN_POINT('Ctrl Pts',(-9.4979812322815,4.58224166307851,-9.51835923202207));
#13362=CARTESIAN_POINT('Ctrl Pts',(-9.50673734385392,5.48871730453454,-9.68608429957861));
#13363=CARTESIAN_POINT('',(-4.12011010549492E-8,10.9774346929669,-9.68608426626665));
#13364=CARTESIAN_POINT('Ctrl Pts',(-9.50673734443727,5.48871736492592,-9.68608431075281));
#13365=CARTESIAN_POINT('Ctrl Pts',(-8.71694238599846,5.93459006657546,-9.51827723663476));
#13366=CARTESIAN_POINT('Ctrl Pts',(-7.92188072226173,6.38395964915516,-9.37991057108432));
#13367=CARTESIAN_POINT('Ctrl Pts',(-6.33211805884209,7.28773429047635,-9.19002022026341));
#13368=CARTESIAN_POINT('Ctrl Pts',(-5.53677988505539,7.74269267835577,-9.13897293541538));
#13369=CARTESIAN_POINT('Ctrl Pts',(-3.94587469694457,8.66117228117376,-9.13860048412926));
#13370=CARTESIAN_POINT('Ctrl Pts',(-3.14812015320142,9.12599280095263,-9.18970703534583));
#13371=CARTESIAN_POINT('Ctrl Pts',(-1.56631645695502,10.0533574210071,-9.3800550537477));
#13372=CARTESIAN_POINT('Ctrl Pts',(-0.781382220745075,10.5161833614735,
-9.51820254214855));
#13373=CARTESIAN_POINT('Ctrl Pts',(-5.20087599329853E-8,10.977434699151,
-9.68608429957861));
#13374=CARTESIAN_POINT('',(9.50673729186498,5.48871738219012,-9.68608426617078));
#13375=CARTESIAN_POINT('Ctrl Pts',(3.04944243361098E-16,10.9774347298519,
-9.68608431075281));
#13376=CARTESIAN_POINT('Ctrl Pts',(0.781034565701908,10.5163885828877,-9.51827723663476));
#13377=CARTESIAN_POINT('Ctrl Pts',(1.56773087177229,10.0525297758065,-9.37991057108433));
#13378=CARTESIAN_POINT('Ctrl Pts',(3.14530400216244,9.12764224395764,-9.19002022026341));
#13379=CARTESIAN_POINT('Ctrl Pts',(3.93697861062418,8.66633837479853,-9.13897293541538));
#13380=CARTESIAN_POINT('Ctrl Pts',(5.52785787357781,7.7478138682911,-9.13860048412926));
#13381=CARTESIAN_POINT('Ctrl Pts',(6.32928152377817,7.2893484273145,-9.18970703534583));
#13382=CARTESIAN_POINT('Ctrl Pts',(7.92330469143948,6.38314855259225,-9.3800550537477));
#13383=CARTESIAN_POINT('Ctrl Pts',(8.71659083151876,5.93478853396749,-9.51820254214855));
#13384=CARTESIAN_POINT('Ctrl Pts',(9.50673729179886,5.48871739464254,-9.68608429956877));
#13385=CARTESIAN_POINT('Ctrl Pts',(9.50673734443727,5.48871736492592,-9.68608431075281));
#13386=CARTESIAN_POINT('Ctrl Pts',(9.49796877532218,4.58095205751653,-9.5181206164762));
#13387=CARTESIAN_POINT('Ctrl Pts',(9.48959593650276,3.66686690783038,-9.3796529749726));
#13388=CARTESIAN_POINT('Ctrl Pts',(9.47740359978457,1.836490901034,-9.18974634775445));
#13389=CARTESIAN_POINT('Ctrl Pts',(9.47374549680553,0.919367531929958,-9.13878618833741));
#13390=CARTESIAN_POINT('Ctrl Pts',(9.47374549680553,1.47832800417317E-13,
-9.13878618833741));
#13391=CARTESIAN_POINT('Origin',(0.,0.,-10.2));
#13392=CARTESIAN_POINT('Origin',(0.,0.,-11.0720179162868));
#13393=CARTESIAN_POINT('',(-12.0720179162868,-1.47839581004301E-15,-12.));
#13394=CARTESIAN_POINT('Origin',(-12.0720179162868,-1.47839581004302E-15,
-11.0720179162868));
#13395=CARTESIAN_POINT('Origin',(0.,0.,-12.));
#13396=CARTESIAN_POINT('Origin',(0.,0.,-12.));
#13397=CARTESIAN_POINT('',(-5.1,-6.2456986756515E-16,-12.));
#13398=CARTESIAN_POINT('Origin',(-2.35299013008461E-16,10.3923048454133,
-12.));
#13399=CARTESIAN_POINT('',(-2.35299013008461E-16,10.3923048454133,-8.93601699627353));
#13400=CARTESIAN_POINT('',(0.,10.3923048454133,-1.2));
#13401=CARTESIAN_POINT('',(-2.35299013008461E-16,10.3923048454133,-12.));
#13402=CARTESIAN_POINT('',(-9.00000000008138,5.19615066621323,-8.93601701787771));
#13403=CARTESIAN_POINT('Ctrl Pts',(-6.07852008438492E-6,10.3923013359781,
-8.93603703387842));
#13404=CARTESIAN_POINT('Ctrl Pts',(-0.301195462062673,10.2184095643127,
-8.87641996617827));
#13405=CARTESIAN_POINT('Ctrl Pts',(-0.602385138153431,10.0445176237446,
-8.82152809836376));
#13406=CARTESIAN_POINT('Ctrl Pts',(-0.903577682885929,9.87062402696534,
-8.77193268574838));
#13407=CARTESIAN_POINT('Ctrl Pts',(-1.19726885426351,9.70106135011187,-8.72357247537563));
#13408=CARTESIAN_POINT('Ctrl Pts',(-1.49096277600334,9.53149708533603,-8.6802482745101));
#13409=CARTESIAN_POINT('Ctrl Pts',(-1.78464966066903,9.36193688341683,-8.64244231384737));
#13410=CARTESIAN_POINT('Ctrl Pts',(-1.93979249065832,9.27236512875967,-8.62247096329028));
#13411=CARTESIAN_POINT('Ctrl Pts',(-2.09493314852878,9.1827946281759,-8.60403870988084));
#13412=CARTESIAN_POINT('Ctrl Pts',(-2.25006873511963,9.09322705549679,-8.58721096889182));
#13413=CARTESIAN_POINT('Ctrl Pts',(-2.57357704286633,8.90644944693415,-8.55211963923506));
#13414=CARTESIAN_POINT('Ctrl Pts',(-2.89698498406969,8.71972978502468,-8.52402127580572));
#13415=CARTESIAN_POINT('Ctrl Pts',(-3.22042421153454,8.53299206003282,-8.50343197405325));
#13416=CARTESIAN_POINT('Ctrl Pts',(-3.54650772650974,8.34472765493547,-8.48267434382096));
#13417=CARTESIAN_POINT('Ctrl Pts',(-3.87262302478416,8.15644489978108,-8.469549024806));
#13418=CARTESIAN_POINT('Ctrl Pts',(-4.19889273693572,7.96807299360913,-8.46453388744621));
#13419=CARTESIAN_POINT('Ctrl Pts',(-4.2877593691349,7.91676581957802,-8.46316790601863));
#13420=CARTESIAN_POINT('Ctrl Pts',(-4.37663738754378,7.86545207170697,-8.46240330115924));
#13421=CARTESIAN_POINT('Ctrl Pts',(-4.46552911497214,7.81413040892396,-8.46224908602198));
#13422=CARTESIAN_POINT('Ctrl Pts',(-4.47702295601336,7.80749443670175,-8.46222914576066));
#13423=CARTESIAN_POINT('Ctrl Pts',(-4.48851325102017,7.80086051178337,-8.46221928455636));
#13424=CARTESIAN_POINT('Ctrl Pts',(-4.50000000003849,7.79422863414232,-8.4622194678316));
#13425=CARTESIAN_POINT('Ctrl Pts',(-5.02158818205606,7.49308955670287,-8.46222778995974));
#13426=CARTESIAN_POINT('Ctrl Pts',(-5.5431711936851,7.19195346442769,-8.48297232998703));
#13427=CARTESIAN_POINT('Ctrl Pts',(-6.06475920079968,6.89081448843259,-8.52296987642172));
#13428=CARTESIAN_POINT('Ctrl Pts',(-6.29317060573264,6.75894110244808,-8.54048541675317));
#13429=CARTESIAN_POINT('Ctrl Pts',(-6.52158273068006,6.62706730087865,-8.56169255024703));
#13430=CARTESIAN_POINT('Ctrl Pts',(-6.74999529948836,6.49519324368519,-8.58646372999425));
#13431=CARTESIAN_POINT('Ctrl Pts',(-6.81977791240305,6.45490423360735,-8.59403160446263));
#13432=CARTESIAN_POINT('Ctrl Pts',(-6.88955873896841,6.4146162548414,-8.60193048700176));
#13433=CARTESIAN_POINT('Ctrl Pts',(-6.95933612940203,6.37433025985928,-8.61015656868989));
#13434=CARTESIAN_POINT('Ctrl Pts',(-7.30266835708907,6.17610730660974,-8.65063212866093));
#13435=CARTESIAN_POINT('Ctrl Pts',(-7.64602887829948,5.97786801610262,-8.69891514178612));
#13436=CARTESIAN_POINT('Ctrl Pts',(-7.98939420141902,5.77962595354147,-8.75415779946613));
#13437=CARTESIAN_POINT('Ctrl Pts',(-8.32626415664962,5.58513399339513,-8.80835544368486));
#13438=CARTESIAN_POINT('Ctrl Pts',(-8.66313875598589,5.3906393526244,-8.86925130743439));
#13439=CARTESIAN_POINT('Ctrl Pts',(-9.00000000000115,5.19615242270862,-8.93599629172134));
#13440=CARTESIAN_POINT('',(-9.,5.19615242270663,-1.2));
#13441=CARTESIAN_POINT('',(-9.,5.19615242270663,-12.));
#13442=CARTESIAN_POINT('',(-4.5,7.79422863405995,0.));
#13443=CARTESIAN_POINT('Ctrl Pts',(-8.99999999999999,5.19615242270665,-1.19999999999999));
#13444=CARTESIAN_POINT('Ctrl Pts',(-6.5884572681199,6.5884572681199,-3.99680288865056E-15));
#13445=CARTESIAN_POINT('Ctrl Pts',(-4.50000000000001,7.79422863405995,-3.78993143111475E-15));
#13446=CARTESIAN_POINT('Ctrl Pts',(-4.50000000000001,7.79422863405995,-3.78993143111475E-15));
#13447=CARTESIAN_POINT('Ctrl Pts',(-2.41154273188011,9.,-3.68820461000181E-15));
#13448=CARTESIAN_POINT('Ctrl Pts',(-1.63323345900868E-14,10.3923048454133,
-1.2));
#13449=CARTESIAN_POINT('Origin',(9.,5.19615242270663,-12.));
#13450=CARTESIAN_POINT('',(9.,5.19615242270663,-8.93601699627312));
#13451=CARTESIAN_POINT('',(9.,5.19615242270664,-1.2));
#13452=CARTESIAN_POINT('',(9.,5.19615242270663,-12.));
#13453=CARTESIAN_POINT('Ctrl Pts',(8.99999392148002,5.19615593214177,-8.93603703387764));
#13454=CARTESIAN_POINT('Ctrl Pts',(8.69880453793134,5.37004770381067,-8.87641996617583));
#13455=CARTESIAN_POINT('Ctrl Pts',(8.39761486183447,5.54393964438233,-8.82152809836008));
#13456=CARTESIAN_POINT('Ctrl Pts',(8.0964223170958,5.71783324116511,-8.77193268574382));
#13457=CARTESIAN_POINT('Ctrl Pts',(7.80273114570837,5.88739591802426,-8.72357247536959));
#13458=CARTESIAN_POINT('Ctrl Pts',(7.50903722395865,6.05696018280582,-8.68024827450306));
#13459=CARTESIAN_POINT('Ctrl Pts',(7.21535033928308,6.22652038473072,-8.6424423138398));
#13460=CARTESIAN_POINT('Ctrl Pts',(7.06020750930979,6.31609213937864,-8.62247096328515));
#13461=CARTESIAN_POINT('Ctrl Pts',(6.90506685145532,6.40566263995317,-8.60403870987786));
#13462=CARTESIAN_POINT('Ctrl Pts',(6.74993126488047,6.49523021262305,-8.58721096889069));
#13463=CARTESIAN_POINT('Ctrl Pts',(6.42642295713265,6.68200782118634,-8.55211963923401));
#13464=CARTESIAN_POINT('Ctrl Pts',(6.10301501593021,6.86872748309998,-8.52402127580485));
#13465=CARTESIAN_POINT('Ctrl Pts',(5.77957578850881,7.05546520816967,-8.50343197405257));
#13466=CARTESIAN_POINT('Ctrl Pts',(5.45349227355191,7.24372961336021,-8.48267434381885));
#13467=CARTESIAN_POINT('Ctrl Pts',(5.12737697532985,7.43201236866678,-8.46954902480367));
#13468=CARTESIAN_POINT('Ctrl Pts',(4.80110726312322,7.62038427480488,-8.46453388744491));
#13469=CARTESIAN_POINT('Ctrl Pts',(4.712240630944,7.67169144880659,-8.46316790601815));
#13470=CARTESIAN_POINT('Ctrl Pts',(4.62336261254755,7.72300519663518,-8.46240330115919));
#13471=CARTESIAN_POINT('Ctrl Pts',(4.53447088512655,7.7743268593669,-8.46224908602198));
#13472=CARTESIAN_POINT('Ctrl Pts',(4.5229770440827,7.78096283158455,-8.46222914576066));
#13473=CARTESIAN_POINT('Ctrl Pts',(4.51148674907318,7.78759675649823,-8.46221928455636));
#13474=CARTESIAN_POINT('Ctrl Pts',(4.5000000000521,7.79422863413447,-8.4622194678316));
#13475=CARTESIAN_POINT('Ctrl Pts',(3.97841181773793,8.0953677114542,-8.46222778995974));
#13476=CARTESIAN_POINT('Ctrl Pts',(3.45682880584612,8.39650380366825,-8.48297233000062));
#13477=CARTESIAN_POINT('Ctrl Pts',(2.93524079883684,8.69764278023972,-8.52296987646097));
#13478=CARTESIAN_POINT('Ctrl Pts',(2.70682939419531,8.829516166335,-8.54048541678485));
#13479=CARTESIAN_POINT('Ctrl Pts',(2.47841726963945,8.96138996818865,-8.56169255026554));
#13480=CARTESIAN_POINT('Ctrl Pts',(2.25000470177625,9.09326402662507,-8.58646372999426));
#13481=CARTESIAN_POINT('Ctrl Pts',(2.18022208909817,9.13355303711273,-8.59403160446263));
#13482=CARTESIAN_POINT('Ctrl Pts',(2.11044126273703,9.17384101623243,-8.60193048700176));
#13483=CARTESIAN_POINT('Ctrl Pts',(2.04066387244898,9.21412701146667,-8.61015656868988));
#13484=CARTESIAN_POINT('Ctrl Pts',(1.69733164548179,9.4123499659547,-8.65063212866048));
#13485=CARTESIAN_POINT('Ctrl Pts',(1.35397112327281,9.61058925472395,-8.69891514178508));
#13486=CARTESIAN_POINT('Ctrl Pts',(1.01060579944003,9.80883131604148,-8.75415779946437));
#13487=CARTESIAN_POINT('Ctrl Pts',(0.673735843502585,10.0033232749718,-8.80835544368355));
#13488=CARTESIAN_POINT('Ctrl Pts',(0.33686124402347,10.1978179155034,-8.86925130743368));
#13489=CARTESIAN_POINT('Ctrl Pts',(1.15152427354714E-12,10.3923048454153,
-8.93599629172134));
#13490=CARTESIAN_POINT('',(4.5,7.79422863405995,0.));
#13491=CARTESIAN_POINT('Ctrl Pts',(1.4874090430258E-14,10.3923048454133,
-1.19999999999999));
#13492=CARTESIAN_POINT('Ctrl Pts',(2.41154273188011,9.,2.99760216648792E-15));
#13493=CARTESIAN_POINT('Ctrl Pts',(4.50000000000001,7.79422863405994,2.1656751034942E-15));
#13494=CARTESIAN_POINT('Ctrl Pts',(4.50000000000001,7.79422863405994,2.1656751034942E-15));
#13495=CARTESIAN_POINT('Ctrl Pts',(6.58845726811989,6.5884572681199,1.23696196253983E-15));
#13496=CARTESIAN_POINT('Ctrl Pts',(8.99999999999997,5.19615242270665,-1.19999999999998));
#13497=CARTESIAN_POINT('Origin',(9.,5.19615242270663,-12.));
#13498=CARTESIAN_POINT('',(9.,-5.19615242270664,-8.93601701652031));
#13499=CARTESIAN_POINT('',(9.,-5.19615242270664,-1.2));
#13500=CARTESIAN_POINT('',(9.,-5.19615242270664,-12.));
#13501=CARTESIAN_POINT('Ctrl Pts',(9.,-5.19614539697823,-8.93603707371988));
#13502=CARTESIAN_POINT('Ctrl Pts',(9.,-4.84829207744338,-8.87640809817269));
#13503=CARTESIAN_POINT('Ctrl Pts',(9.,-4.5004384103798,-8.82150625311342));
#13504=CARTESIAN_POINT('Ctrl Pts',(9.,-4.15258143955633,-8.77190307482733));
#13505=CARTESIAN_POINT('Ctrl Pts',(9.,-3.81338948504499,-8.72353549733419));
#13506=CARTESIAN_POINT('Ctrl Pts',(9.,-3.47419436295703,-8.68020598944004));
#13507=CARTESIAN_POINT('Ctrl Pts',(9.,-3.13500738320275,-8.64239703270597));
#13508=CARTESIAN_POINT('Ctrl Pts',(9.,-2.95600024043739,-8.62244322044345));
#13509=CARTESIAN_POINT('Ctrl Pts',(9.,-2.77699560569171,-8.60402620280014));
#13510=CARTESIAN_POINT('Ctrl Pts',(9.,-2.59799681666225,-8.58721124573255));
#13511=CARTESIAN_POINT('Ctrl Pts',(9.,-2.22450410506814,-8.55212573512904));
#13512=CARTESIAN_POINT('Ctrl Pts',(9.00000000000212,-1.85112676034851,-8.52403085874111));
#13513=CARTESIAN_POINT('Ctrl Pts',(9.0000000000486,-1.47771346656234,-8.50344248169531));
#13514=CARTESIAN_POINT('Ctrl Pts',(9.00000000009545,-1.10129661789082,-8.48268850175993));
#13515=CARTESIAN_POINT('Ctrl Pts',(9.00000000017784,-0.724843258692337,
-8.46956223116017));
#13516=CARTESIAN_POINT('Ctrl Pts',(9.00000000014829,-0.348212540979102,
-8.46454110270077));
#13517=CARTESIAN_POINT('Ctrl Pts',(9.00000000014023,-0.245516126139824,
-8.46317198471072));
#13518=CARTESIAN_POINT('Ctrl Pts',(9.0000000001243,-0.142806604662479,-8.46240519271688));
#13519=CARTESIAN_POINT('Ctrl Pts',(9.00000000010304,-0.0400813005700133,
-8.46224976049714));
#13520=CARTESIAN_POINT('Ctrl Pts',(9.00000000010027,-0.0267167643637567,
-8.46222953880448));
#13521=CARTESIAN_POINT('Ctrl Pts',(9.00000000009742,-0.0133563304832161,
-8.46221953990594));
#13522=CARTESIAN_POINT('Ctrl Pts',(9.00000000009451,-8.15016804301746E-12,
-8.46221972848024));
#13523=CARTESIAN_POINT('Ctrl Pts',(8.99999999995155,0.654989413214678,-8.46222897609269));
#13524=CARTESIAN_POINT('Ctrl Pts',(8.99999999976969,1.30997129101454,-8.48676659793625));
#13525=CARTESIAN_POINT('Ctrl Pts',(9.00000000024692,1.96496169710869,-8.53391508241261));
#13526=CARTESIAN_POINT('Ctrl Pts',(9.00000000040068,2.17599761070563,-8.54910618048611));
#13527=CARTESIAN_POINT('Ctrl Pts',(9.0000000006655,2.3870340834294,-8.56664433473375));
#13528=CARTESIAN_POINT('Ctrl Pts',(9.00000000130499,2.59807069766354,-8.58646463712839));
#13529=CARTESIAN_POINT('Ctrl Pts',(9.00000000154905,2.67861189655562,-8.59402896866896));
#13530=CARTESIAN_POINT('Ctrl Pts',(9.00000000175971,2.75915062264558,-8.60192400520041));
#13531=CARTESIAN_POINT('Ctrl Pts',(9.00000000190986,2.83968469038153,-8.61014594910981));
#13532=CARTESIAN_POINT('Ctrl Pts',(9.0000000026465,3.23477341913773,-8.65048164130054));
#13533=CARTESIAN_POINT('Ctrl Pts',(9.0000000016216,3.62990043667534,-8.6985717486516));
#13534=CARTESIAN_POINT('Ctrl Pts',(9.00000000088224,4.02503435673907,-8.75357741709708));
#13535=CARTESIAN_POINT('Ctrl Pts',(9.00000000015179,4.41540872345877,-8.80792051925833));
#13536=CARTESIAN_POINT('Ctrl Pts',(9.00000000000588,4.80578984875463,-8.86901301455119));
#13537=CARTESIAN_POINT('Ctrl Pts',(9.00000000000233,5.19615242270663,-8.93599629172134));
#13538=CARTESIAN_POINT('',(9.,0.,0.));
#13539=CARTESIAN_POINT('Ctrl Pts',(9.,0.,1.62425632676704E-15));
#13540=CARTESIAN_POINT('Ctrl Pts',(9.,2.4115427318801,1.49904191230263E-15));
#13541=CARTESIAN_POINT('Ctrl Pts',(9.,5.19615242270662,-1.19999999999999));
#13542=CARTESIAN_POINT('Ctrl Pts',(9.,-5.19615242270662,-1.19999999999999));
#13543=CARTESIAN_POINT('Ctrl Pts',(9.,-2.4115427318801,1.33226762955019E-15));
#13544=CARTESIAN_POINT('Ctrl Pts',(9.,0.,1.62425632676704E-15));
#13545=CARTESIAN_POINT('Origin',(0.,-10.3923048454133,-12.));
#13546=CARTESIAN_POINT('',(0.,-10.3923048454133,-8.93601699627358));
#13547=CARTESIAN_POINT('',(-1.30104260698261E-14,-10.3923048454133,-1.2));
#13548=CARTESIAN_POINT('',(0.,-10.3923048454133,-12.));
#13549=CARTESIAN_POINT('Ctrl Pts',(6.07852010015009E-6,-10.3923013359781,
-8.93603703387852));
#13550=CARTESIAN_POINT('Ctrl Pts',(0.30119546205775,-10.2184095643155,-8.87641996617938));
#13551=CARTESIAN_POINT('Ctrl Pts',(0.602385138143551,-10.0445176237503,
-8.82152809836565));
#13552=CARTESIAN_POINT('Ctrl Pts',(0.903577682871094,-9.87062402697391,
-8.77193268575082));
#13553=CARTESIAN_POINT('Ctrl Pts',(1.1972688542489,-9.70106135012032,-8.72357247537779));
#13554=CARTESIAN_POINT('Ctrl Pts',(1.49096277598897,-9.53149708534433,-8.68024827451193));
#13555=CARTESIAN_POINT('Ctrl Pts',(1.78464966065489,-9.361936883425,-8.64244231384889));
#13556=CARTESIAN_POINT('Ctrl Pts',(1.93979249064888,-9.27236512876513,-8.62247096329104));
#13557=CARTESIAN_POINT('Ctrl Pts',(2.09493314852404,-9.18279462817865,-8.60403870988093));
#13558=CARTESIAN_POINT('Ctrl Pts',(2.25006873511959,-9.09322705549682,-8.58721096889136));
#13559=CARTESIAN_POINT('Ctrl Pts',(2.57357704286724,-8.90644944693363,-8.55211963923438));
#13560=CARTESIAN_POINT('Ctrl Pts',(2.89698498407157,-8.7197297850236,-8.52402127580505));
#13561=CARTESIAN_POINT('Ctrl Pts',(3.22042421153739,-8.53299206003118,-8.5034319740527));
#13562=CARTESIAN_POINT('Ctrl Pts',(3.54650772651119,-8.34472765493464,-8.48267434382068));
#13563=CARTESIAN_POINT('Ctrl Pts',(3.87262302478421,-8.15644489978106,-8.46954902480601));
#13564=CARTESIAN_POINT('Ctrl Pts',(4.19889273693436,-7.96807299360993,-8.46453388744643));
#13565=CARTESIAN_POINT('Ctrl Pts',(4.28775936913399,-7.91676581957855,-8.46316790601889));
#13566=CARTESIAN_POINT('Ctrl Pts',(4.37663738754333,-7.86545207170724,-8.46240330115955));
#13567=CARTESIAN_POINT('Ctrl Pts',(4.46552911497214,-7.81413040892397,-8.46224908602234));
#13568=CARTESIAN_POINT('Ctrl Pts',(4.47702295601336,-7.80749443670175,-8.46222914576103));
#13569=CARTESIAN_POINT('Ctrl Pts',(4.48851325102017,-7.80086051178337,-8.46221928455673));
#13570=CARTESIAN_POINT('Ctrl Pts',(4.50000000003849,-7.79422863414233,-8.46221946783198));
#13571=CARTESIAN_POINT('Ctrl Pts',(5.02158818224417,-7.49308955659427,-8.46222778996038));
#13572=CARTESIAN_POINT('Ctrl Pts',(5.54317119406134,-7.19195346421047,-8.48297233000241));
#13573=CARTESIAN_POINT('Ctrl Pts',(6.06475920136405,-6.89081448810676,-8.52296987646522));
#13574=CARTESIAN_POINT('Ctrl Pts',(6.29317060610888,-6.75894110223086,-8.54048541678825));
#13575=CARTESIAN_POINT('Ctrl Pts',(6.52158273086818,-6.62706730077005,-8.56169255026751));
#13576=CARTESIAN_POINT('Ctrl Pts',(6.74999529948835,-6.4951932436852,-8.58646372999432));
#13577=CARTESIAN_POINT('Ctrl Pts',(6.81977791240305,-6.45490423360736,-8.59403160446269));
#13578=CARTESIAN_POINT('Ctrl Pts',(6.88955873896841,-6.4146162548414,-8.60193048700183));
#13579=CARTESIAN_POINT('Ctrl Pts',(6.95933612940203,-6.37433025985929,-8.61015656868998));
#13580=CARTESIAN_POINT('Ctrl Pts',(7.30266835710366,-6.17610730660132,-8.65063212866286));
#13581=CARTESIAN_POINT('Ctrl Pts',(7.64602887832874,-5.97786801608574,-8.69891514179043));
#13582=CARTESIAN_POINT('Ctrl Pts',(7.98939420146296,-5.77962595351611,-8.75415779947333));
#13583=CARTESIAN_POINT('Ctrl Pts',(8.32626415667892,-5.58513399337823,-8.80835544369024));
#13584=CARTESIAN_POINT('Ctrl Pts',(8.66313875600055,-5.39063935261595,-8.8692513074373));
#13585=CARTESIAN_POINT('Ctrl Pts',(9.00000000000115,-5.19615242270863,-8.93599629172134));
#13586=CARTESIAN_POINT('',(4.5,-7.79422863405995,0.));
#13587=CARTESIAN_POINT('Ctrl Pts',(8.99999999999998,-5.19615242270664,-1.19999999999999));
#13588=CARTESIAN_POINT('Ctrl Pts',(6.58845726811989,-6.5884572681199,-2.44249065417534E-15));
#13589=CARTESIAN_POINT('Ctrl Pts',(4.5,-7.79422863405995,-2.97780326730443E-15));
#13590=CARTESIAN_POINT('Ctrl Pts',(4.5,-7.79422863405995,-2.97780326730443E-15));
#13591=CARTESIAN_POINT('Ctrl Pts',(2.41154273188012,-9.,-3.41478402099401E-15));
#13592=CARTESIAN_POINT('Ctrl Pts',(2.42068530531642E-14,-10.3923048454133,
-1.19999999999999));
#13593=CARTESIAN_POINT('Origin',(-9.,-5.19615242270664,-12.));
#13594=CARTESIAN_POINT('',(-9.,-5.19615242270664,-8.93601699627313));
#13595=CARTESIAN_POINT('',(-9.,-5.19615242270664,-1.2));
#13596=CARTESIAN_POINT('',(-9.,-5.19615242270664,-12.));
#13597=CARTESIAN_POINT('Ctrl Pts',(-8.99999392148003,-5.19615593214178,
-8.93603703387762));
#13598=CARTESIAN_POINT('Ctrl Pts',(-8.69880453793641,-5.37004770380774,
-8.87641996617677));
#13599=CARTESIAN_POINT('Ctrl Pts',(-8.3976148618446,-5.54393964437648,-8.82152809836176));
#13600=CARTESIAN_POINT('Ctrl Pts',(-8.09642231711102,-5.71783324115633,
-8.77193268574606));
#13601=CARTESIAN_POINT('Ctrl Pts',(-7.80273114573057,-5.88739591801145,
-8.72357247537269));
#13602=CARTESIAN_POINT('Ctrl Pts',(-7.50903722398783,-6.05696018278898,
-8.68024827450678));
#13603=CARTESIAN_POINT('Ctrl Pts',(-7.21535033931923,-6.22652038470985,
-8.64244231384387));
#13604=CARTESIAN_POINT('Ctrl Pts',(-7.06020750933391,-6.31609213936472,
-8.62247096328738));
#13605=CARTESIAN_POINT('Ctrl Pts',(-6.90506685146741,-6.4056626399462,-8.6040387098785));
#13606=CARTESIAN_POINT('Ctrl Pts',(-6.74993126488053,-6.49523021262302,
-8.58721096888999));
#13607=CARTESIAN_POINT('Ctrl Pts',(-6.4264229571074,-6.68200782120092,-8.5521196392305));
#13608=CARTESIAN_POINT('Ctrl Pts',(-6.10301501587966,-6.86872748312918,
-8.5240212757998));
#13609=CARTESIAN_POINT('Ctrl Pts',(-5.77957578843295,-7.05546520821348,
-8.50343197404727));
#13610=CARTESIAN_POINT('Ctrl Pts',(-5.45349227348263,-7.24372961340022,
-8.48267434381534));
#13611=CARTESIAN_POINT('Ctrl Pts',(-5.12737697526716,-7.43201236870298,
-8.46954902480175));
#13612=CARTESIAN_POINT('Ctrl Pts',(-4.80110726306711,-7.62038427483728,
-8.46453388744425));
#13613=CARTESIAN_POINT('Ctrl Pts',(-4.71224063090659,-7.67169144882819,
-8.46316790601809));
#13614=CARTESIAN_POINT('Ctrl Pts',(-4.62336261252885,-7.72300519664598,
-8.46240330115948));
#13615=CARTESIAN_POINT('Ctrl Pts',(-4.53447088512656,-7.7743268593669,-8.46224908602235));
#13616=CARTESIAN_POINT('Ctrl Pts',(-4.5229770440827,-7.78096283158455,-8.46222914576104));
#13617=CARTESIAN_POINT('Ctrl Pts',(-4.51148674907318,-7.78759675649824,
-8.46221928455675));
#13618=CARTESIAN_POINT('Ctrl Pts',(-4.50000000005209,-7.79422863413447,
-8.46221946783199));
#13619=CARTESIAN_POINT('Ctrl Pts',(-3.97841181786548,-8.09536771138056,
-8.46222778996039));
#13620=CARTESIAN_POINT('Ctrl Pts',(-3.45682880610124,-8.39650380352096,
-8.48297232999122));
#13621=CARTESIAN_POINT('Ctrl Pts',(-2.9352407992195,-8.69764278001881,-8.52296987643228));
#13622=CARTESIAN_POINT('Ctrl Pts',(-2.70682939445042,-8.82951616618772,
-8.54048541676178));
#13623=CARTESIAN_POINT('Ctrl Pts',(-2.47841726976704,-8.961389968115,-8.56169255025224));
#13624=CARTESIAN_POINT('Ctrl Pts',(-2.25000470177628,-9.09326402662505,
-8.58646372999467));
#13625=CARTESIAN_POINT('Ctrl Pts',(-2.1802220890982,-9.13355303711272,-8.59403160446301));
#13626=CARTESIAN_POINT('Ctrl Pts',(-2.11044126273707,-9.17384101623242,
-8.6019304870021));
#13627=CARTESIAN_POINT('Ctrl Pts',(-2.04066387244902,-9.21412701146666,
-8.61015656869019));
#13628=CARTESIAN_POINT('Ctrl Pts',(-1.69733164547995,-9.41234996595577,
-8.65063212866084));
#13629=CARTESIAN_POINT('Ctrl Pts',(-1.35397112326908,-9.61058925472611,
-8.69891514178567));
#13630=CARTESIAN_POINT('Ctrl Pts',(-1.01060579943443,-9.80883131604472,
-8.75415779946531));
#13631=CARTESIAN_POINT('Ctrl Pts',(-0.67373584349885,-10.003323274974,-8.80835544368422));
#13632=CARTESIAN_POINT('Ctrl Pts',(-0.336861244021614,-10.1978179155045,
-8.86925130743406));
#13633=CARTESIAN_POINT('Ctrl Pts',(-1.15285654227901E-12,-10.3923048454153,
-8.93599629172134));
#13634=CARTESIAN_POINT('',(-4.5,-7.79422863405995,0.));
#13635=CARTESIAN_POINT('Ctrl Pts',(-2.36235553892334E-14,-10.3923048454133,
-1.19999999999999));
#13636=CARTESIAN_POINT('Ctrl Pts',(-2.41154273188012,-9.,-1.33226762955019E-15));
#13637=CARTESIAN_POINT('Ctrl Pts',(-4.5,-7.79422863405995,-1.0828375517471E-15));
#13638=CARTESIAN_POINT('Ctrl Pts',(-4.5,-7.79422863405995,-1.0828375517471E-15));
#13639=CARTESIAN_POINT('Ctrl Pts',(-6.58845726811989,-6.58845726811991,
-1.18980142210385E-15));
#13640=CARTESIAN_POINT('Ctrl Pts',(-8.99999999999998,-5.19615242270665,
-1.19999999999999));
#13641=CARTESIAN_POINT('Origin',(-9.,5.19615242270663,-12.));
#13642=CARTESIAN_POINT('Ctrl Pts',(-9.,5.19614539650958,-8.93603707639091));
#13643=CARTESIAN_POINT('Ctrl Pts',(-9.,4.84832857664298,-8.87641436251837));
#13644=CARTESIAN_POINT('Ctrl Pts',(-9.,4.50051141122661,-8.82151779810304));
#13645=CARTESIAN_POINT('Ctrl Pts',(-9.,4.15269093788426,-8.77191875049037));
#13646=CARTESIAN_POINT('Ctrl Pts',(-9.,3.81353345495309,-8.72355504152739));
#13647=CARTESIAN_POINT('Ctrl Pts',(-9.,3.47437280046155,-8.68022834191494));
#13648=CARTESIAN_POINT('Ctrl Pts',(-9.,3.13522028344948,-8.64242098329983));
#13649=CARTESIAN_POINT('Ctrl Pts',(-9.,2.9561421598243,-8.62245807428277));
#13650=CARTESIAN_POINT('Ctrl Pts',(-9.,2.7770665453474,-8.60403315443626));
#13651=CARTESIAN_POINT('Ctrl Pts',(-9.,2.59799678343793,-8.58721156446757));
#13652=CARTESIAN_POINT('Ctrl Pts',(-9.,2.22433287352971,-8.55211004307419));
#13653=CARTESIAN_POINT('Ctrl Pts',(-9.00000000000195,1.85078513355755,-8.52400542530791));
#13654=CARTESIAN_POINT('Ctrl Pts',(-9.00000000004448,1.4772011518465,-8.50341433154624));
#13655=CARTESIAN_POINT('Ctrl Pts',(-9.00000000008736,1.10053656913797,-8.48265344211055));
#13656=CARTESIAN_POINT('Ctrl Pts',(-9.00000000016269,0.723835163596231,
-8.46953046790419));
#13657=CARTESIAN_POINT('Ctrl Pts',(-9.00000000013545,0.346954913253201,
-8.46452392492529));
#13658=CARTESIAN_POINT('Ctrl Pts',(-9.00000000012805,0.244465457900586,
-8.46316243712475));
#13659=CARTESIAN_POINT('Ctrl Pts',(-9.00000000011348,0.141962856303526,
-8.46240089073438));
#13660=CARTESIAN_POINT('Ctrl Pts',(-9.00000000009406,0.0394444306228228,
-8.46224826955939));
#13661=CARTESIAN_POINT('Ctrl Pts',(-9.00000000009157,0.0262922197916786,
-8.46222868960723));
#13662=CARTESIAN_POINT('Ctrl Pts',(-9.00000000008901,0.013144076632877,
-8.46221900508837));
#13663=CARTESIAN_POINT('Ctrl Pts',(-9.00000000008638,7.53135263285704E-12,
-8.46221918237743));
#13664=CARTESIAN_POINT('Ctrl Pts',(-8.99999999997667,-0.549916859676629,
-8.46222659972942));
#13665=CARTESIAN_POINT('Ctrl Pts',(-8.99999999993513,-1.09982934347759,
-8.47951821623097));
#13666=CARTESIAN_POINT('Ctrl Pts',(-9.00000000008774,-1.64974515680917,
-8.51297261954941));
#13667=CARTESIAN_POINT('Ctrl Pts',(-9.00000000017546,-1.96585272030167,
-8.53220318114577));
#13668=CARTESIAN_POINT('Ctrl Pts',(-9.00000000032562,-2.28196122532694,
-8.5567735078678));
#13669=CARTESIAN_POINT('Ctrl Pts',(-9.0000000012242,-2.5980708693782,-8.58646281049615));
#13670=CARTESIAN_POINT('Ctrl Pts',(-9.0000000014534,-2.67869870244963,-8.59403544923519));
#13671=CARTESIAN_POINT('Ctrl Pts',(-9.00000000165122,-2.75932489265377,
-8.60193950572842));
#13672=CARTESIAN_POINT('Ctrl Pts',(-9.0000000017922,-2.83994782092948,-8.61017115770036));
#13673=CARTESIAN_POINT('Ctrl Pts',(-9.00000000248791,-3.23780289414195,
-8.65079241232356));
#13674=CARTESIAN_POINT('Ctrl Pts',(-9.00000000150868,-3.63568481736304,
-8.69927635641474));
#13675=CARTESIAN_POINT('Ctrl Pts',(-9.00000000081449,-4.03357090898489,
-8.75476582106047));
#13676=CARTESIAN_POINT('Ctrl Pts',(-9.00000000013838,-4.42109951253233,
-8.80881082338287));
#13677=CARTESIAN_POINT('Ctrl Pts',(-9.00000000000569,-4.80863209974855,
-8.86950072341166));
#13678=CARTESIAN_POINT('Ctrl Pts',(-9.00000000000228,-5.19615242270664,
-8.93599629172134));
#13679=CARTESIAN_POINT('',(-9.,0.,0.));
#13680=CARTESIAN_POINT('Ctrl Pts',(-9.,-5.19615242270662,-1.19999999999999));
#13681=CARTESIAN_POINT('Ctrl Pts',(-9.,-2.4115427318801,3.66373598126302E-15));
#13682=CARTESIAN_POINT('Ctrl Pts',(-9.,1.08283755047889E-14,1.62425632571833E-15));
#13683=CARTESIAN_POINT('Ctrl Pts',(-9.,1.08283755047889E-14,1.62425632571833E-15));
#13684=CARTESIAN_POINT('Ctrl Pts',(-9.,2.41154273188011,-7.86239849479496E-16));
#13685=CARTESIAN_POINT('Ctrl Pts',(-9.,5.19615242270663,-1.2));
#13686=CARTESIAN_POINT('Origin',(-18.,-3.46944695195361E-15,0.));
#13687=CARTESIAN_POINT('Origin',(0.,0.,0.));
#13688=CARTESIAN_POINT('Origin',(0.,0.,0.));
#13689=CARTESIAN_POINT('Origin',(0.,0.,0.));
#13690=CARTESIAN_POINT('Origin',(0.,0.,0.));
#13691=CARTESIAN_POINT('Origin',(0.,0.,0.));
#13692=CARTESIAN_POINT('Origin',(0.,0.,0.));
#13693=CARTESIAN_POINT('Origin',(-18.,-3.46944695195361E-15,-12.));
#13694=CARTESIAN_POINT('Origin',(0.,0.,0.));
#13695=CARTESIAN_POINT('Origin',(0.,0.,0.));
#13696=CARTESIAN_POINT('Origin',(0.,0.,0.));
#13697=CARTESIAN_POINT('Origin',(0.,0.,0.));
#13698=CARTESIAN_POINT('Origin',(0.,0.,0.));
#13699=CARTESIAN_POINT('Origin',(0.,0.,0.));
#13700=CARTESIAN_POINT('Ctrl Pts',(-9.41651585048208,-4.95567688430906,
-9.02143340818646));
#13701=CARTESIAN_POINT('Ctrl Pts',(-9.33347922663126,-5.00361810144193,
-9.54376732265014));
#13702=CARTESIAN_POINT('Ctrl Pts',(-9.56264608596435,-5.45717682649977,
-9.69801774536269));
#13703=CARTESIAN_POINT('Ctrl Pts',(-7.82828519779296,-5.87264227917434,
-8.68478716584893));
#13704=CARTESIAN_POINT('Ctrl Pts',(-7.78096540982093,-5.89996237149985,
-9.20046647829273));
#13705=CARTESIAN_POINT('Ctrl Pts',(-7.99064761656677,-6.34458248438458,
-9.36117071967683));
#13706=CARTESIAN_POINT('Ctrl Pts',(-6.20942222566736,-6.80729325191217,
-8.46511979781123));
#13707=CARTESIAN_POINT('Ctrl Pts',(-6.17732188361541,-6.82582639303532,
-8.96938931321266));
#13708=CARTESIAN_POINT('Ctrl Pts',(-6.40309790806795,-7.24276319894628,
-9.14170490909588));
#13709=CARTESIAN_POINT('Ctrl Pts',(-3.69699523786471,-8.25784364963932,
-8.4607958473145));
#13710=CARTESIAN_POINT('Ctrl Pts',(-3.7121972466429,-8.24906676577982,-8.96490808900259));
#13711=CARTESIAN_POINT('Ctrl Pts',(-3.95417133760969,-8.65630407204171,
-9.13738096492018));
#13712=CARTESIAN_POINT('Ctrl Pts',(-2.86553968521064,-8.73788473678336,
-8.51288388844084));
#13713=CARTESIAN_POINT('Ctrl Pts',(-2.89372401459971,-8.72161250662362,
-9.01926238740844));
#13714=CARTESIAN_POINT('Ctrl Pts',(-3.14556979243607,-9.12747462876032,
-9.18946890902302));
#13715=CARTESIAN_POINT('Ctrl Pts',(-1.21577897758477,-9.69037452542962,
-8.70732652632404));
#13716=CARTESIAN_POINT('Ctrl Pts',(-1.27236213191392,-9.65770622604611,
-9.22034895088592));
#13717=CARTESIAN_POINT('Ctrl Pts',(-1.53900867015813,-10.0694227766623,
-9.38391126097275));
#13718=CARTESIAN_POINT('Ctrl Pts',(-0.396828014250257,-10.1631960845639,
-8.84899630416932));
#13719=CARTESIAN_POINT('Ctrl Pts',(-0.465016578930744,-10.1238273983887,
-9.36716113818611));
#13720=CARTESIAN_POINT('Ctrl Pts',(-0.74038577260122,-10.5403775350051,
-9.5255700245206));
#13721=CARTESIAN_POINT('Ctrl Pts',(0.417977369734739,-10.6336241923448,
-9.02174323061994));
#13722=CARTESIAN_POINT('Ctrl Pts',(0.334920910614397,-10.5856715233137,
-9.54408615058461));
#13723=CARTESIAN_POINT('Ctrl Pts',(0.0566989198404312,-11.0109268220334,
-9.6983275674176));
#13724=CARTESIAN_POINT('Ctrl Pts',(-9.5067372390073,-5.48871738714607,-9.68608418865576));
#13725=CARTESIAN_POINT('Ctrl Pts',(-9.4675108481587,-5.46606999446181,-9.66959818350506));
#13726=CARTESIAN_POINT('Ctrl Pts',(-9.42925913707253,-5.4439810970595,-9.64980240749262));
#13727=CARTESIAN_POINT('Ctrl Pts',(-9.39245990190791,-5.42272474549804,
-9.62687223341926));
#13728=CARTESIAN_POINT('Ctrl Pts',(-9.35128004286391,-5.3989380130517,-9.60121242467673));
#13729=CARTESIAN_POINT('Ctrl Pts',(-9.31191221316965,-5.37619344504106,
-9.57162843008722));
#13730=CARTESIAN_POINT('Ctrl Pts',(-9.2749983072906,-5.35488193328893,-9.5383540974491));
#13731=CARTESIAN_POINT('Ctrl Pts',(-9.248186554751,-5.33940269949517,-9.51418588356417));
#13732=CARTESIAN_POINT('Ctrl Pts',(-9.22266843593477,-5.32467985874466,
-9.48806920949896));
#13733=CARTESIAN_POINT('Ctrl Pts',(-9.19871798627596,-5.31086441980473,
-9.46010057379183));
#13734=CARTESIAN_POINT('Ctrl Pts',(-9.18229304117869,-5.30138994941625,
-9.4409200025508));
#13735=CARTESIAN_POINT('Ctrl Pts',(-9.16660604341306,-5.29234227360425,
-9.42086846723453));
#13736=CARTESIAN_POINT('Ctrl Pts',(-9.15175721629724,-5.28376928889603,
-9.39998581131754));
#13737=CARTESIAN_POINT('Ctrl Pts',(-9.13182856474318,-5.27226346263139,
-9.37195914159832));
#13738=CARTESIAN_POINT('Ctrl Pts',(-9.11351521748966,-5.26164700778255,
-9.34258220711578));
#13739=CARTESIAN_POINT('Ctrl Pts',(-9.09700209817711,-5.25207548543112,
-9.31197696571696));
#13740=CARTESIAN_POINT('Ctrl Pts',(-9.08187618167217,-5.24330802937557,
-9.28394275139018));
#13741=CARTESIAN_POINT('Ctrl Pts',(-9.06826135533797,-5.23541758926273,
-9.2548764399327));
#13742=CARTESIAN_POINT('Ctrl Pts',(-9.05633367221833,-5.2285208428221,-9.22490110097916));
#13743=CARTESIAN_POINT('Ctrl Pts',(-9.04538493587851,-5.22219013654632,
-9.1973859432065));
#13744=CARTESIAN_POINT('Ctrl Pts',(-9.03585874901313,-5.21669683169049,
-9.16910418723661));
#13745=CARTESIAN_POINT('Ctrl Pts',(-9.02790971986095,-5.2121260329523,-9.14019098056147));
#13746=CARTESIAN_POINT('Ctrl Pts',(-9.02027081268773,-5.20773355852555,
-9.11240578847789));
#13747=CARTESIAN_POINT('Ctrl Pts',(-9.01408944739803,-5.20419309163258,
-9.08403702004755));
#13748=CARTESIAN_POINT('Ctrl Pts',(-9.00950634701575,-5.20157374064314,
-9.0552511510112));
#13749=CARTESIAN_POINT('Ctrl Pts',(-9.0051246078554,-5.19906947238633,-9.02773000613096));
#13750=CARTESIAN_POINT('Ctrl Pts',(-9.002204824453,-5.19740715548407,-8.99982768780994));
#13751=CARTESIAN_POINT('Ctrl Pts',(-9.00085816830124,-5.1966406953204,-8.97173538759073));
#13752=CARTESIAN_POINT('Ctrl Pts',(-9.00028875667948,-5.19631661012298,
-8.95985701596189));
#13753=CARTESIAN_POINT('Ctrl Pts',(-9.00000036310671,-5.19615261240624,
-8.94794524541767));
#13754=CARTESIAN_POINT('Ctrl Pts',(-9.00000000034277,-5.19615242287113,
-8.93601699624085));
#13755=CARTESIAN_POINT('Ctrl Pts',(-2.90734818439019E-11,-10.3923048457926,
-8.93601699624128));
#13756=CARTESIAN_POINT('Ctrl Pts',(-4.10642892561727E-8,-10.3923058149047,
-8.96427557571348));
#13757=CARTESIAN_POINT('Ctrl Pts',(-1.27558244240631E-5,-10.3941683544014,
-8.9924385290414));
#13758=CARTESIAN_POINT('Ctrl Pts',(-3.18146852205633E-5,-10.3977787368057,
-9.02029415413065));
#13759=CARTESIAN_POINT('Ctrl Pts',(-5.15275647690907E-5,-10.4015130121237,
-9.04910566537449));
#13760=CARTESIAN_POINT('Ctrl Pts',(-7.7414908830901E-5,-10.4071161272311,
-9.07758819694581));
#13761=CARTESIAN_POINT('Ctrl Pts',(-9.83587654872778E-5,-10.4144403013317,
-9.10555931636106));
#13762=CARTESIAN_POINT('Ctrl Pts',(-0.000120807532366093,-10.4222907502563,
-9.13554028640848));
#13763=CARTESIAN_POINT('Ctrl Pts',(-0.000136929653821073,-10.4321173156833,
-9.16493372802667));
#13764=CARTESIAN_POINT('Ctrl Pts',(-0.000138635033354084,-10.4437307211343,
-9.1935757361048));
#13765=CARTESIAN_POINT('Ctrl Pts',(-0.000140425004800706,-10.4559201861495,
-9.22363847325004));
#13766=CARTESIAN_POINT('Ctrl Pts',(-0.000125857207500358,-10.4700770096022,
-9.252874295224));
#13767=CARTESIAN_POINT('Ctrl Pts',(-0.000100780446528402,-10.4859934580781,
-9.2811507783596));
#13768=CARTESIAN_POINT('Ctrl Pts',(-7.31620606961085E-5,-10.5035230989907,
-9.31229319033588));
#13769=CARTESIAN_POINT('Ctrl Pts',(-3.24759853636551E-5,-10.5231860217892,
-9.34227343310186));
#13770=CARTESIAN_POINT('Ctrl Pts',(-1.17901018813735E-5,-10.5447373137949,
-9.37096347131022));
#13771=CARTESIAN_POINT('Ctrl Pts',(-4.70298657794152E-6,-10.5521209235649,
-9.38079286095251));
#13772=CARTESIAN_POINT('Ctrl Pts',(-1.81298691785883E-7,-10.5597265189714,
-9.39047108282798));
#13773=CARTESIAN_POINT('Ctrl Pts',(-1.77170306928887E-7,-10.5675452688574,
-9.39999358405634));
#13774=CARTESIAN_POINT('Ctrl Pts',(-1.64365910958916E-7,-10.5917955199845,
-9.42952810677552));
#13775=CARTESIAN_POINT('Ctrl Pts',(-1.40786991299795E-5,-10.6179922639664,
-9.45742229073908));
#13776=CARTESIAN_POINT('Ctrl Pts',(-2.3249300100427E-5,-10.6458168703524,
-9.4835474262003));
#13777=CARTESIAN_POINT('Ctrl Pts',(-3.45972702524547E-5,-10.6802478529868,
-9.51587543375258));
#13778=CARTESIAN_POINT('Ctrl Pts',(-3.8706976771203E-5,-10.7171709180177,
-9.5454959152349));
#13779=CARTESIAN_POINT('Ctrl Pts',(-3.39070251259832E-5,-10.7560291195714,
-9.57222637923024));
#13780=CARTESIAN_POINT('Ctrl Pts',(-2.8201444964252E-5,-10.8022188731966,
-9.60400020037645));
#13781=CARTESIAN_POINT('Ctrl Pts',(-1.27781523534252E-5,-10.8511471894092,
-9.63169251308496));
#13782=CARTESIAN_POINT('Ctrl Pts',(-5.34813184271594E-6,-10.9019135377996,
-9.65503883152351));
#13783=CARTESIAN_POINT('Ctrl Pts',(-1.72253203311199E-6,-10.9266858063004,
-9.6664310487541));
#13784=CARTESIAN_POINT('Ctrl Pts',(5.95818053386175E-8,-10.9518957124607,
-9.67678873846151));
#13785=CARTESIAN_POINT('Ctrl Pts',(7.20244415219895E-8,-10.9774346496439,
-9.68608418837616));
#13786=CARTESIAN_POINT('Ctrl Pts',(-0.416515850482077,-10.6327803838108,
-9.02143340818646));
#13787=CARTESIAN_POINT('Ctrl Pts',(-0.333479226631307,-10.584839166678,
-9.54376732264983));
#13788=CARTESIAN_POINT('Ctrl Pts',(-0.0552692782898434,-11.0100828510945,
-9.69801774536257));
#13789=CARTESIAN_POINT('Ctrl Pts',(1.17171480220768,-9.7158149889452,-8.68478716585303));
#13790=CARTESIAN_POINT('Ctrl Pts',(1.21903459018144,-9.68849489662272,-9.20046647830121));
#13791=CARTESIAN_POINT('Ctrl Pts',(1.4992457995972,-10.0923950708269,-9.36117071967617));
#13792=CARTESIAN_POINT('Ctrl Pts',(2.79057777433264,-8.78116401620774,-8.46511979781123));
#13793=CARTESIAN_POINT('Ctrl Pts',(2.82267811638498,-8.76263087508485,-8.96938931321236));
#13794=CARTESIAN_POINT('Ctrl Pts',(3.07086796984993,-9.16662705077884,-9.14170490909608));
#13795=CARTESIAN_POINT('Ctrl Pts',(5.30300476213529,-7.33061361848059,-8.4607958473145));
#13796=CARTESIAN_POINT('Ctrl Pts',(5.28780275335659,-7.33939050234015,-8.9649080890023));
#13797=CARTESIAN_POINT('Ctrl Pts',(5.51949356046498,-7.75256486530674,-9.13738096491987));
#13798=CARTESIAN_POINT('Ctrl Pts',(6.13446031478957,-6.85057253133643,-8.51288388844));
#13799=CARTESIAN_POINT('Ctrl Pts',(6.1062759854001,-6.86684476149545,-9.01926238740732));
#13800=CARTESIAN_POINT('Ctrl Pts',(6.33184000468667,-7.28788066400649,-9.18946890902303));
#13801=CARTESIAN_POINT('Ctrl Pts',(7.78422102241503,-5.8980827426904,-8.70732652632487));
#13802=CARTESIAN_POINT('Ctrl Pts',(7.72763786808632,-5.93075104207461,-9.22034895088645));
#13803=CARTESIAN_POINT('Ctrl Pts',(7.95087159095549,-6.36753199333221,-9.38391126097247));
#13804=CARTESIAN_POINT('Ctrl Pts',(8.60317198574983,-5.42526118355596,-8.84899630416909));
#13805=CARTESIAN_POINT('Ctrl Pts',(8.53498342106806,-5.4646298697288,-9.36716113818546));
#13806=CARTESIAN_POINT('Ctrl Pts',(8.75804182449227,-5.91138165517438,-9.52557002452023));
#13807=CARTESIAN_POINT('Ctrl Pts',(9.41797736973474,-4.95483307577511,-9.02174323061993));
#13808=CARTESIAN_POINT('Ctrl Pts',(9.33492091061444,-5.00278574480615,-9.5440861505843));
#13809=CARTESIAN_POINT('Ctrl Pts',(9.56409180701241,-5.45636070606741,-9.69832756741748));
#13810=CARTESIAN_POINT('Ctrl Pts',(9.00000000031458,-5.19615242292188,-8.93601701648795));
#13811=CARTESIAN_POINT('Ctrl Pts',(9.00000081983887,-5.1961529434644,-8.96427559612485));
#13812=CARTESIAN_POINT('Ctrl Pts',(9.00160746974801,-5.19709522496851,-8.99243854955995));
#13813=CARTESIAN_POINT('Ctrl Pts',(9.00472462396319,-5.198916922074,-9.02029417470534));
#13814=CARTESIAN_POINT('Ctrl Pts',(9.00794874561115,-5.20080113205156,-9.04910568605485));
#13815=CARTESIAN_POINT('Ctrl Pts',(9.01278824276164,-5.20362510916489,-9.07758821767627));
#13816=CARTESIAN_POINT('Ctrl Pts',(9.01912069246065,-5.20730533458325,-9.10555933709354));
#13817=CARTESIAN_POINT('Ctrl Pts',(9.02590815713673,-5.21125000074161,-9.13554030717923));
#13818=CARTESIAN_POINT('Ctrl Pts',(9.03441015222614,-5.21617724611114,-9.16493374877919));
#13819=CARTESIAN_POINT('Ctrl Pts',(9.04446680453275,-5.22198542622267,-9.19357575679092));
#13820=CARTESIAN_POINT('Ctrl Pts',(9.05502229682808,-5.22808170941394,-9.22363849393975));
#13821=CARTESIAN_POINT('Ctrl Pts',(9.06728975039373,-5.23514750557975,-9.25287431586034));
#13822=CARTESIAN_POINT('Ctrl Pts',(9.0810863384078,-5.24308401322878,-9.28115079889175));
#13823=CARTESIAN_POINT('Ctrl Pts',(9.09628126293037,-5.25182491602132,-9.31229321069587));
#13824=CARTESIAN_POINT('Ctrl Pts',(9.11333019759206,-5.26162114280348,-9.34227345323255));
#13825=CARTESIAN_POINT('Ctrl Pts',(9.13200450784775,-5.27237887486722,-9.37096349115774));
#13826=CARTESIAN_POINT('Ctrl Pts',(9.13840244098876,-5.27606453980212,-9.38079287398074));
#13827=CARTESIAN_POINT('Ctrl Pts',(9.14499133635352,-5.27986341912618,-9.39047108923729));
#13828=CARTESIAN_POINT('Ctrl Pts',(9.1517625698874,-5.28377278786267,-9.39999358405638));
#13829=CARTESIAN_POINT('Ctrl Pts',(9.17276390981393,-5.29589790233735,-9.42952810677569));
#13830=CARTESIAN_POINT('Ctrl Pts',(9.19544399843216,-5.30900832449442,-9.45742229073938));
#13831=CARTESIAN_POINT('Ctrl Pts',(9.21953622911234,-5.32292856966092,-9.4835474262007));
#13832=CARTESIAN_POINT('Ctrl Pts',(9.24934866076502,-5.3401538886081,-9.51587543375205));
#13833=CARTESIAN_POINT('Ctrl Pts',(9.28132291821314,-5.35861898023332,-9.54549591523359));
#13834=CARTESIAN_POINT('Ctrl Pts',(9.31497750787883,-5.37804392412957,-9.57222637922831));
#13835=CARTESIAN_POINT('Ctrl Pts',(9.35498186070127,-5.40113385976393,-9.6040002003735));
#13836=CARTESIAN_POINT('Ctrl Pts',(9.39736273715034,-5.42558466090601,-9.63169251308128));
#13837=CARTESIAN_POINT('Ctrl Pts',(9.4413313995222,-5.45096140051353,-9.65503883151944));
#13838=CARTESIAN_POINT('Ctrl Pts',(9.46278662615571,-5.46334439490381,-9.66643104875163));
#13839=CARTESIAN_POINT('Ctrl Pts',(9.48461993637701,-5.47594780462949,-9.67678873846038));
#13840=CARTESIAN_POINT('Ctrl Pts',(9.50673731098735,-5.4887172624469,-9.68608418837614));
#13841=CARTESIAN_POINT('Ctrl Pts',(-9.,5.67710804811706,-9.02143424315509));
#13842=CARTESIAN_POINT('Ctrl Pts',(-9.,5.58122826343245,-9.54375341158405));
#13843=CARTESIAN_POINT('Ctrl Pts',(-9.50735826663105,5.55291153619582,-9.69801293012095));
#13844=CARTESIAN_POINT('Ctrl Pts',(-9.,3.84304933649568,-8.68476431765287));
#13845=CARTESIAN_POINT('Ctrl Pts',(-9.0000000000016,3.78841469353132,-9.20042897477229));
#13846=CARTESIAN_POINT('Ctrl Pts',(-9.48987412151624,3.74769245548026,-9.3611418811313));
#13847=CARTESIAN_POINT('Ctrl Pts',(-9.,1.97362405991046,-8.46509342346937));
#13848=CARTESIAN_POINT('Ctrl Pts',(-9.,1.93656169730459,-8.96934796476675));
#13849=CARTESIAN_POINT('Ctrl Pts',(-9.47394637335796,1.92362385779232,-9.14167211079771));
#13850=CARTESIAN_POINT('Ctrl Pts',(-9.,-0.927645358236382,-8.46080823523173));
#13851=CARTESIAN_POINT('Ctrl Pts',(-9.,-0.910084670211163,-8.96490692122887));
#13852=CARTESIAN_POINT('Ctrl Pts',(-9.47364809996973,-0.904144222134296,
-9.13738692201634));
#13853=CARTESIAN_POINT('Ctrl Pts',(-9.,-1.88752338654127,-8.5129006820434));
#13854=CARTESIAN_POINT('Ctrl Pts',(-9.,-1.85497578383212,-9.0192656693921));
#13855=CARTESIAN_POINT('Ctrl Pts',(-9.47739316073685,-1.83980071118508,
-9.18947936857881));
#13856=CARTESIAN_POINT('Ctrl Pts',(-9.,-3.7923825728723,-8.7073405558973));
#13857=CARTESIAN_POINT('Ctrl Pts',(-9.,-3.72704613553677,-9.22034905417095));
#13858=CARTESIAN_POINT('Ctrl Pts',(-9.48986299758601,-3.70198073363909,
-9.38391924329362));
#13859=CARTESIAN_POINT('Ctrl Pts',(-9.,-4.73797542141407,-8.84900381462939));
#13860=CARTESIAN_POINT('Ctrl Pts',(-9.00000000000247,-4.65923931810371,
-9.36715420610053));
#13861=CARTESIAN_POINT('Ctrl Pts',(-9.49840964046578,-4.62903686950057,
-9.52557170693384));
#13862=CARTESIAN_POINT('Ctrl Pts',(-9.,-5.67878800057612,-9.02174265850467));
#13863=CARTESIAN_POINT('Ctrl Pts',(-9.,-5.58288541678637,-9.54407079115471));
#13864=CARTESIAN_POINT('Ctrl Pts',(-9.5073742726743,-5.55456408813261,-9.69832134547053));
#13865=CARTESIAN_POINT('Ctrl Pts',(-9.50673731098736,5.48871726244691,-9.68608418837615));
#13866=CARTESIAN_POINT('Ctrl Pts',(-9.46751090700237,5.46606991294245,-9.66959818674222));
#13867=CARTESIAN_POINT('Ctrl Pts',(-9.4292555139926,5.44398741281737,-9.64980241574297));
#13868=CARTESIAN_POINT('Ctrl Pts',(-9.39244736393246,5.42274652050346,-9.62687224800763));
#13869=CARTESIAN_POINT('Ctrl Pts',(-9.35125753785235,5.39897709284228,-9.60121245202594));
#13870=CARTESIAN_POINT('Ctrl Pts',(-9.31187626544443,5.37625584557009,-9.57162847358945));
#13871=CARTESIAN_POINT('Ctrl Pts',(-9.27496301517173,5.35494322921267,-9.53835416024961));
#13872=CARTESIAN_POINT('Ctrl Pts',(-9.24815172482378,5.33946318502768,-9.51418594776514));
#13873=CARTESIAN_POINT('Ctrl Pts',(-9.22264230677134,5.324725264057,-9.48806927473095));
#13874=CARTESIAN_POINT('Ctrl Pts',(-9.19870255635967,5.31089128345573,-9.46010063975213));
#13875=CARTESIAN_POINT('Ctrl Pts',(-9.1822849306166,5.30140408696692,-9.44092004790256));
#13876=CARTESIAN_POINT('Ctrl Pts',(-9.16660589513319,5.29234257523934,-9.42086848991658));
#13877=CARTESIAN_POINT('Ctrl Pts',(-9.15175704158874,5.28376959610175,-9.39998580942839));
#13878=CARTESIAN_POINT('Ctrl Pts',(-9.13182837913581,5.27226379149956,-9.3719591412876));
#13879=CARTESIAN_POINT('Ctrl Pts',(-9.1134775869241,5.26171219558187,-9.34258220859915));
#13880=CARTESIAN_POINT('Ctrl Pts',(-9.09693184649301,5.25219717637988,-9.31197696915498));
#13881=CARTESIAN_POINT('Ctrl Pts',(-9.08177604900606,5.24348147672834,-9.28394275618111));
#13882=CARTESIAN_POINT('Ctrl Pts',(-9.06813531450727,5.23563591146739,-9.25487644617962));
#13883=CARTESIAN_POINT('Ctrl Pts',(-9.05619871536813,5.22875460811564,-9.22490110874421));
#13884=CARTESIAN_POINT('Ctrl Pts',(-9.04524179434031,5.22243807720807,-9.19738595126647));
#13885=CARTESIAN_POINT('Ctrl Pts',(-9.03572135889103,5.21693480952055,-9.16910419558254));
#13886=CARTESIAN_POINT('Ctrl Pts',(-9.02778841599091,5.21233614735411,-9.14019098916249));
#13887=CARTESIAN_POINT('Ctrl Pts',(-9.02016496747924,5.20791689655528,-9.11240579730802));
#13888=CARTESIAN_POINT('Ctrl Pts',(-9.01400815004361,5.20433391022739,-9.0840370290776));
#13889=CARTESIAN_POINT('Ctrl Pts',(-9.00944817481981,5.20167450390064,-9.05525116019153));
#13890=CARTESIAN_POINT('Ctrl Pts',(-9.00508854480459,5.19913194016382,-9.02773001548115));
#13891=CARTESIAN_POINT('Ctrl Pts',(-9.00218904391566,5.19743449151929,-8.99982769728534));
#13892=CARTESIAN_POINT('Ctrl Pts',(-9.00085194133044,5.1966514826345,-8.97173539712726));
#13893=CARTESIAN_POINT('Ctrl Pts',(-9.0002865694687,5.19632040019114,-8.95985702951628));
#13894=CARTESIAN_POINT('Ctrl Pts',(-9.00000034626581,5.19615264266129,-8.947945263001));
#13895=CARTESIAN_POINT('Ctrl Pts',(-9.00000000031462,5.19615242292189,-8.93601701784535));
#13896=CARTESIAN_POINT('Ctrl Pts',(9.,-5.67710138297224,-9.02143301966492));
#13897=CARTESIAN_POINT('Ctrl Pts',(9.,-5.58121904513111,-9.54376655404368));
#13898=CARTESIAN_POINT('Ctrl Pts',(9.5073763234892,-5.55290396848635,-9.69801721577213));
#13899=CARTESIAN_POINT('Ctrl Pts',(9.,-3.84322958818909,-8.68479770034242));
#13900=CARTESIAN_POINT('Ctrl Pts',(9.,-3.78858774329166,-9.20047677759492));
#13901=CARTESIAN_POINT('Ctrl Pts',(9.48989350969518,-3.74786882415842,-9.3611811508237));
#13902=CARTESIAN_POINT('Ctrl Pts',(9.,-1.97401147132877,-8.46514012239073));
#13903=CARTESIAN_POINT('Ctrl Pts',(9.,-1.93694391502001,-8.96941003041365));
#13904=CARTESIAN_POINT('Ctrl Pts',(9.47396685145451,-1.92400102339044,-9.14172507325324));
#13905=CARTESIAN_POINT('Ctrl Pts',(9.,0.926883757386691,-8.46078630815419));
#13906=CARTESIAN_POINT('Ctrl Pts',(9.,0.909336207055026,-8.96489785481209));
#13907=CARTESIAN_POINT('Ctrl Pts',(9.47366379315207,0.903401719775828,-9.13737126521503));
#13908=CARTESIAN_POINT('Ctrl Pts',(9.,1.88715353767526,-8.51287122562915));
#13909=CARTESIAN_POINT('Ctrl Pts',(9.,1.85461215070573,-9.01924893473238));
#13910=CARTESIAN_POINT('Ctrl Pts',(9.47740850275143,1.83943906473165,-9.18945608808641));
#13911=CARTESIAN_POINT('Ctrl Pts',(9.,3.79222649301937,-8.70731633004835));
#13912=CARTESIAN_POINT('Ctrl Pts',(9.,3.72689115576847,-9.22033807316646));
#13913=CARTESIAN_POINT('Ctrl Pts',(9.48987919364789,3.70182678106926,-9.383900913727));
#13914=CARTESIAN_POINT('Ctrl Pts',(9.,4.73790659517861,-8.84899105760459));
#13915=CARTESIAN_POINT('Ctrl Pts',(9.,4.65916993880134,-9.36715542952161));
#13916=CARTESIAN_POINT('Ctrl Pts',(9.49842686847536,4.62896805034413,-9.52556463079721));
#13917=CARTESIAN_POINT('Ctrl Pts',(9.,5.67879329673354,-9.02174363091134));
#13918=CARTESIAN_POINT('Ctrl Pts',(9.,5.58288799679954,-9.54408619370965));
#13919=CARTESIAN_POINT('Ctrl Pts',(9.50739244391453,5.55456828647369,-9.6983278266485));
#13920=CARTESIAN_POINT('Ctrl Pts',(9.0000000003434,5.19615242287113,-8.9360169962408));
#13921=CARTESIAN_POINT('Ctrl Pts',(9.00000086053094,5.19615287188961,-8.96427557554858));
#13922=CARTESIAN_POINT('Ctrl Pts',(9.00162022478813,5.19707313031505,-8.99243852866675));
#13923=CARTESIAN_POINT('Ctrl Pts',(9.00475643740047,5.19886181605305,-9.0202941535193));
#13924=CARTESIAN_POINT('Ctrl Pts',(9.00800027144488,5.20071188185179,-9.04910566453395));
#13925=CARTESIAN_POINT('Ctrl Pts',(9.01286565539748,5.2034910203135,-9.07758819584685));
#13926=CARTESIAN_POINT('Ctrl Pts',(9.01921904834677,5.20713496946256,-9.10555931499254));
#13927=CARTESIAN_POINT('Ctrl Pts',(9.02602896110547,5.21104075271889,-9.13554028463599));
#13928=CARTESIAN_POINT('Ctrl Pts',(9.03454707754073,5.21594007325843,-9.16493372584192));
#13929=CARTESIAN_POINT('Ctrl Pts',(9.0446054343648,5.22174529904746,-9.19357573352205));
#13930=CARTESIAN_POINT('Ctrl Pts',(9.05516271560771,5.2278384813043,-9.22363846998386));
#13931=CARTESIAN_POINT('Ctrl Pts',(9.06741560021868,5.23492950897316,-9.25287429130466));
#13932=CARTESIAN_POINT('Ctrl Pts',(9.08118711020269,5.24290945012497,-9.28115077384541));
#13933=CARTESIAN_POINT('Ctrl Pts',(9.09635441441848,5.25169818826729,-9.31229318403473));
#13934=CARTESIAN_POINT('Ctrl Pts',(9.11336266082172,5.26156488415088,-9.34227342516874));
#13935=CARTESIAN_POINT('Ctrl Pts',(9.13201628280739,5.27235844388821,-9.37096346195156));
#13936=CARTESIAN_POINT('Ctrl Pts',(9.13840713436601,5.27605638727547,-9.38079285414313));
#13937=CARTESIAN_POINT('Ctrl Pts',(9.1449915139327,5.27986310181482,-9.39047107849866));
#13938=CARTESIAN_POINT('Ctrl Pts',(9.15176274956368,5.2837724813323,-9.39999358213585));
#13939=CARTESIAN_POINT('Ctrl Pts',(9.17276407693867,5.2958976182429,-9.42952810540652));
#13940=CARTESIAN_POINT('Ctrl Pts',(9.19545808017158,5.30898394063489,-9.45742228997671));
#13941=CARTESIAN_POINT('Ctrl Pts',(9.21955948177444,5.32288830241885,-9.48354742602077));
#13942=CARTESIAN_POINT('Ctrl Pts',(9.24938325823851,5.3400939647514,-9.51587543043768));
#13943=CARTESIAN_POINT('Ctrl Pts',(9.28136162178356,5.35855193648451,-9.5454959093921));
#13944=CARTESIAN_POINT('Ctrl Pts',(9.31501140762171,5.37798519202097,-9.57222637143016));
#13945=CARTESIAN_POINT('Ctrl Pts',(9.35501003305752,5.40108499755732,-9.60400017658687));
#13946=CARTESIAN_POINT('Ctrl Pts',(9.39737546199132,5.4255624983292,-9.63169247761706));
#13947=CARTESIAN_POINT('Ctrl Pts',(9.44133666898288,5.45095209217556,-9.65503878908946));
#13948=CARTESIAN_POINT('Ctrl Pts',(9.46278829527576,5.46334138073684,-9.66643102290868));
#13949=CARTESIAN_POINT('Ctrl Pts',(9.48461984970672,5.47594789224658,-9.6767887266977));
#13950=CARTESIAN_POINT('Ctrl Pts',(9.50673723892373,5.48871738724752,-9.68608418809832));
#13951=CARTESIAN_POINT('Ctrl Pts',(0.416515850482078,10.6327803838108,-9.02143340818645));
#13952=CARTESIAN_POINT('Ctrl Pts',(0.333479226631358,10.584839166678,-9.54376732264953));
#13953=CARTESIAN_POINT('Ctrl Pts',(0.0552692782900587,11.0100828510942,
-9.69801774536245));
#13954=CARTESIAN_POINT('Ctrl Pts',(-1.17171480220777,9.71581498894514,-8.68478716585237));
#13955=CARTESIAN_POINT('Ctrl Pts',(-1.21903459018308,9.68849489662884,-9.20046647829118));
#13956=CARTESIAN_POINT('Ctrl Pts',(-1.49924579959968,10.0923950708306,-9.36117071967749));
#13957=CARTESIAN_POINT('Ctrl Pts',(-2.79057777433264,8.78116401620773,-8.46511979781291));
#13958=CARTESIAN_POINT('Ctrl Pts',(-2.82267811638496,8.76263087508485,-8.96938931321375));
#13959=CARTESIAN_POINT('Ctrl Pts',(-3.07086796985,9.16662705077899,-9.14170490909614));
#13960=CARTESIAN_POINT('Ctrl Pts',(-5.30300476213529,7.33061361848059,-8.46079584731366));
#13961=CARTESIAN_POINT('Ctrl Pts',(-5.28780275335659,7.33939050234014,-8.96490808900116));
#13962=CARTESIAN_POINT('Ctrl Pts',(-5.51949356046466,7.75256486530618,-9.13738096491964));
#13963=CARTESIAN_POINT('Ctrl Pts',(-6.13446031478939,6.85057253133653,-8.51288388844));
#13964=CARTESIAN_POINT('Ctrl Pts',(-6.10627598540037,6.86684476149594,-9.01926238740701));
#13965=CARTESIAN_POINT('Ctrl Pts',(-6.33184000468647,7.28788066400655,-9.18946890902299));
#13966=CARTESIAN_POINT('Ctrl Pts',(-7.78422102241521,5.8980827426903,-8.70732652632487));
#13967=CARTESIAN_POINT('Ctrl Pts',(-7.72763786808578,5.93075104207426,-9.22034895088613));
#13968=CARTESIAN_POINT('Ctrl Pts',(-7.95087159095534,6.36753199333147,-9.38391126097224));
#13969=CARTESIAN_POINT('Ctrl Pts',(-8.60317198574941,5.42526118355619,-8.84899630417094));
#13970=CARTESIAN_POINT('Ctrl Pts',(-8.53498342106766,5.4646298697288,-9.36716113818699));
#13971=CARTESIAN_POINT('Ctrl Pts',(-8.75804182449212,5.91138165517439,-9.52557002452018));
#13972=CARTESIAN_POINT('Ctrl Pts',(-9.41797736973474,4.95483307577511,-9.02174323061993));
#13973=CARTESIAN_POINT('Ctrl Pts',(-9.33492091061449,5.00278574480612,-9.54408615058399));
#13974=CARTESIAN_POINT('Ctrl Pts',(-9.56409180701224,5.45636070606705,-9.69832756741736));
#13975=CARTESIAN_POINT('Ctrl Pts',(-7.20244197616182E-8,10.977434649644,
-9.68608418837618));
#13976=CARTESIAN_POINT('Ctrl Pts',(-5.00286340846749E-8,10.9321399125021,
-9.66959818672784));
#13977=CARTESIAN_POINT('Ctrl Pts',(3.64038997071435E-6,10.8879685202237,
-9.64980241570864));
#13978=CARTESIAN_POINT('Ctrl Pts',(1.25630774211914E-5,10.8454712810141,
-9.62687224794793));
#13979=CARTESIAN_POINT('Ctrl Pts',(2.25479297814334E-5,10.7979151314145,
-9.60121245195519));
#13980=CARTESIAN_POINT('Ctrl Pts',(3.60067895874637E-5,10.7524493254351,
-9.57162847350616));
#13981=CARTESIAN_POINT('Ctrl Pts',(3.53647383512323E-5,10.7098252047811,
-9.5383541601524));
#13982=CARTESIAN_POINT('Ctrl Pts',(3.48983957240436E-5,10.6788659241417,
-9.51418594766149));
#13983=CARTESIAN_POINT('Ctrl Pts',(2.61934615827083E-5,10.6494051595904,
-9.48806927462073));
#13984=CARTESIAN_POINT('Ctrl Pts',(1.54900307618859E-5,10.6217557372769,
-9.46010063963534));
#13985=CARTESIAN_POINT('Ctrl Pts',(8.14973197026581E-6,10.6027940581112,
-9.44092004782107));
#13986=CARTESIAN_POINT('Ctrl Pts',(1.68120725248121E-7,10.5846848592506,
-9.42086848987401));
#13987=CARTESIAN_POINT('Ctrl Pts',(1.77173693458057E-7,10.5675388853301,
-9.39998580942819));
#13988=CARTESIAN_POINT('Ctrl Pts',(1.89323691907141E-7,10.5445272551391,
-9.37195914135774));
#13989=CARTESIAN_POINT('Ctrl Pts',(3.76353141956738E-5,10.5233592049939,
-9.34258220874644));
#13990=CARTESIAN_POINT('Ctrl Pts',(7.02571832642839E-5,10.5042726638926,
-9.31197696938525));
#13991=CARTESIAN_POINT('Ctrl Pts',(0.000100138618398514,10.486789507466,
-9.28394275488897));
#13992=CARTESIAN_POINT('Ctrl Pts',(0.000126047045856005,10.4710535014604,
-9.25487644325188));
#13993=CARTESIAN_POINT('Ctrl Pts',(0.000134963100562419,10.4572754511472,
-9.22490110408888));
#13994=CARTESIAN_POINT('Ctrl Pts',(0.000143147383229936,10.4446282139908,
-9.19738594667423));
#13995=CARTESIAN_POINT('Ctrl Pts',(0.000137395485180129,10.4336316414396,
-9.16910419106805));
#13996=CARTESIAN_POINT('Ctrl Pts',(0.000121308674796911,10.4244621805141,
-9.14019098474074));
#13997=CARTESIAN_POINT('Ctrl Pts',(0.000105849472287728,10.4156504552578,
-9.11240579294972));
#13998=CARTESIAN_POINT('Ctrl Pts',(8.13010084074135E-5,10.408527002,-9.08403702479553));
#13999=CARTESIAN_POINT('Ctrl Pts',(5.81751825992234E-5,10.403248244655,
-9.0552511559988));
#14000=CARTESIAN_POINT('Ctrl Pts',(3.60654036386653E-5,10.3982014126389,
-9.02773001138921));
#14001=CARTESIAN_POINT('Ctrl Pts',(1.57822010900823E-5,10.3948416470749,
-8.9998276933066));
#14002=CARTESIAN_POINT('Ctrl Pts',(6.22790905404415E-6,10.3932921779994,
-8.9717353932735));
#14003=CARTESIAN_POINT('Ctrl Pts',(2.18803160560752E-6,10.3926370101281,
-8.95985701976865));
#14004=CARTESIAN_POINT('Ctrl Pts',(1.73508680193248E-8,10.3923052548651,
-8.94794524732802));
#14005=CARTESIAN_POINT('Ctrl Pts',(2.91081211519974E-11,10.3923048457926,
-8.93601699624122));
#14006=CARTESIAN_POINT('Ctrl Pts',(9.41651585048208,4.95567688430906,-9.02143340818645));
#14007=CARTESIAN_POINT('Ctrl Pts',(9.33347922663135,5.00361810144187,-9.54376732264957));
#14008=CARTESIAN_POINT('Ctrl Pts',(9.56264608596402,5.45717682649912,-9.69801774536247));
#14009=CARTESIAN_POINT('Ctrl Pts',(7.82828519779331,5.87264227917413,-8.68478716584893));
#14010=CARTESIAN_POINT('Ctrl Pts',(7.78096540982123,5.89996237149757,-9.20046647828723));
#14011=CARTESIAN_POINT('Ctrl Pts',(7.99064761656545,6.34458248438075,-9.3611707196757));
#14012=CARTESIAN_POINT('Ctrl Pts',(6.20942222566664,6.80729325191259,-8.46511979781291));
#14013=CARTESIAN_POINT('Ctrl Pts',(6.17732188361544,6.82582639303698,-8.96938931321379));
#14014=CARTESIAN_POINT('Ctrl Pts',(6.40309790806782,7.24276319894767,-9.14170490909629));
#14015=CARTESIAN_POINT('Ctrl Pts',(3.69699523786507,8.2578436496391,-8.46079584731366));
#14016=CARTESIAN_POINT('Ctrl Pts',(3.71219724664288,8.24906676577899,-8.96490808900122));
#14017=CARTESIAN_POINT('Ctrl Pts',(3.95417133760926,8.65630407204012,-9.13738096491959));
#14018=CARTESIAN_POINT('Ctrl Pts',(2.86553968521059,8.73788473678338,-8.51288388844));
#14019=CARTESIAN_POINT('Ctrl Pts',(2.89372401460009,8.72161250662446,-9.01926238740707));
#14020=CARTESIAN_POINT('Ctrl Pts',(3.14556979243603,9.12747462876021,-9.18946890902297));
#14021=CARTESIAN_POINT('Ctrl Pts',(1.21577897758481,9.69037452542958,-8.70732652632487));
#14022=CARTESIAN_POINT('Ctrl Pts',(1.27236213191344,9.65770622604531,-9.2203489508862));
#14023=CARTESIAN_POINT('Ctrl Pts',(1.53900867015742,10.0694227766613,-9.38391126097231));
#14024=CARTESIAN_POINT('Ctrl Pts',(0.396828014250648,10.1631960845637,-8.84899630417139));
#14025=CARTESIAN_POINT('Ctrl Pts',(0.465016578932603,10.1238273983911,-9.36716113818768));
#14026=CARTESIAN_POINT('Ctrl Pts',(0.740385772601153,10.540377535005,-9.52557002452055));
#14027=CARTESIAN_POINT('Ctrl Pts',(-0.417977369734738,10.6336241923448,
-9.02174323061993));
#14028=CARTESIAN_POINT('Ctrl Pts',(-0.334920910614486,10.5856715233138,
-9.54408615058404));
#14029=CARTESIAN_POINT('Ctrl Pts',(-0.0566989198408205,11.0109268220328,
-9.69832756741738));
#14071=UNCERTAINTY_MEASURE_WITH_UNIT(LENGTH_MEASURE(0.01),#14085,
'DISTANCE_ACCURACY_VALUE',
'Maximum model space distance between geometric entities at asserted c
onnectivities');
#14073=UNCERTAINTY_MEASURE_WITH_UNIT(LENGTH_MEASURE(0.01),#14085,
'DISTANCE_ACCURACY_VALUE',
'Maximum model space distance between geometric entities at asserted c
onnectivities');
#14082=(
GEOMETRIC_REPRESENTATION_CONTEXT(3)
GLOBAL_UNCERTAINTY_ASSIGNED_CONTEXT((#14071))
GLOBAL_UNIT_ASSIGNED_CONTEXT((#14085,#14087,#14088))
REPRESENTATION_CONTEXT('','3D')
);
#14084=(
GEOMETRIC_REPRESENTATION_CONTEXT(3)
GLOBAL_UNCERTAINTY_ASSIGNED_CONTEXT((#14073))
GLOBAL_UNIT_ASSIGNED_CONTEXT((#14085,#14087,#14088))
REPRESENTATION_CONTEXT('','3D')
);
#14085=(
LENGTH_UNIT()
NAMED_UNIT(*)
SI_UNIT(.MILLI.,.METRE.)
);
#14087=(
NAMED_UNIT(*)
PLANE_ANGLE_UNIT()
SI_UNIT($,.RADIAN.)
);
#14088=(
NAMED_UNIT(*)
SI_UNIT($,.STERADIAN.)
SOLID_ANGLE_UNIT()
);
#14097=SHAPE_DEFINITION_REPRESENTATION(#14107,#14127);
#14107=PRODUCT_DEFINITION_SHAPE('',$,#14138);
#14127=SHAPE_REPRESENTATION('',(#3802),#14082);
#14129=PRODUCT_DEFINITION_CONTEXT('part definition',#14161,'design');
#14138=PRODUCT_DEFINITION(
'hex flange nut gradea_iso_ISO - 4161 - M12 - N',
'hex flange nut gradea_iso_ISO - 4161 - M12 - N',#14148,#14129);
#14148=PRODUCT_DEFINITION_FORMATION('',$,#14171);
#14161=APPLICATION_CONTEXT(
'Core Data for Automotive Mechanical Design Process');
#14162=PRODUCT_CONTEXT('part definition',#14161,'mechanical');
#14171=PRODUCT('hex flange nut gradea_iso_ISO - 4161 - M12 - N',
'hex flange nut gradea_iso_ISO - 4161 - M12 - N',$,(#14162));
#14177=PRESENTATION_STYLE_ASSIGNMENT((#14183));
#14183=SURFACE_STYLE_USAGE(.BOTH.,#14189);
#14189=SURFACE_SIDE_STYLE('',(#14195));
#14195=SURFACE_STYLE_FILL_AREA(#14201);
#14201=FILL_AREA_STYLE('Opaque(31,36,43)',(#14207));
#14207=FILL_AREA_STYLE_COLOUR('Opaque(31,36,43)',#14213);
#14213=COLOUR_RGB('Opaque(31,36,43)',0.12156862745098,0.141176470588235,
0.168627450980392);
ENDSEC;
END-ISO-10303-21;
